ISO-10303-21;
HEADER;
/* Generated by software containing ST-Developer
 * from STEP Tools, Inc. (www.steptools.com) 
 */

FILE_DESCRIPTION(
/* description */ (''),
/* implementation_level */ '2;1');

FILE_NAME(
/* name */ '06_Set_Screw_ISO_4026_M2x2.5.step',
/* time_stamp */ '2026-10-25T01:35:35-07:00',
/* author */ (''),
/* organization */ (''),
/* preprocessor_version */ 'ST-DEVELOPER v20.2',
/* originating_system */ 'Autodesk Translation Framework v15.15.0.0',
/* authorisation */ '');

FILE_SCHEMA (('AUTOMOTIVE_DESIGN { 1 0 10303 214 3 1 1 }'));
ENDSEC;

DATA;
#10=MECHANICAL_DESIGN_GEOMETRIC_PRESENTATION_REPRESENTATION('',(#265),#11430);
#80=B_SPLINE_SURFACE_WITH_KNOTS('',3,3,((#7470,#7471,#7472,#7473,#7474,
#7475,#7476,#7477,#7478,#7479,#7480,#7481,#7482,#7483,#7484,#7485,#7486,
#7487,#7488,#7489,#7490,#7491,#7492,#7493,#7494,#7495,#7496,#7497,#7498,
#7499,#7500,#7501,#7502,#7503,#7504,#7505,#7506,#7507,#7508),(#7509,#7510,
#7511,#7512,#7513,#7514,#7515,#7516,#7517,#7518,#7519,#7520,#7521,#7522,
#7523,#7524,#7525,#7526,#7527,#7528,#7529,#7530,#7531,#7532,#7533,#7534,
#7535,#7536,#7537,#7538,#7539,#7540,#7541,#7542,#7543,#7544,#7545,#7546,
#7547),(#7548,#7549,#7550,#7551,#7552,#7553,#7554,#7555,#7556,#7557,#7558,
#7559,#7560,#7561,#7562,#7563,#7564,#7565,#7566,#7567,#7568,#7569,#7570,
#7571,#7572,#7573,#7574,#7575,#7576,#7577,#7578,#7579,#7580,#7581,#7582,
#7583,#7584,#7585,#7586),(#7587,#7588,#7589,#7590,#7591,#7592,#7593,#7594,
#7595,#7596,#7597,#7598,#7599,#7600,#7601,#7602,#7603,#7604,#7605,#7606,
#7607,#7608,#7609,#7610,#7611,#7612,#7613,#7614,#7615,#7616,#7617,#7618,
#7619,#7620,#7621,#7622,#7623,#7624,#7625)),.UNSPECIFIED.,.F.,.F.,.F.,(4,
4),(4,1,1,1,1,1,1,1,1,1,1,1,1,1,1,1,1,1,1,1,1,1,1,1,1,1,1,1,1,1,1,1,1,1,
1,1,4),(0.,0.0262983047615875),(8.30929135176533,9.30907769871814,10.308864045671,
11.3086503926238,12.3084367395766,13.3082230865294,14.3080094334822,15.307795780435,
16.3075821273878,17.3073684743406,18.3071548212935,19.3069411682463,20.3067275151991,
21.3065138621519,22.3063002091047,23.3060865560575,24.3058729030103,25.3056592499631,
26.305445596916,27.3052319438688,28.3050182908216,29.3048046377744,30.3045909847272,
31.30437733168,32.3041636786328,33.3039500255856,34.3037363725385,35.3035227194913,
36.3033090664441,37.3030954133969,38.3028817603497,39.3026681073025,40.3024544542553,
41.3022408012082,42.302027148161,43.3018134951138,44.3015998420666),
 .UNSPECIFIED.);
#81=B_SPLINE_SURFACE_WITH_KNOTS('',3,3,((#7807,#7808,#7809,#7810,#7811,
#7812,#7813,#7814,#7815,#7816,#7817,#7818,#7819,#7820,#7821,#7822,#7823,
#7824,#7825,#7826,#7827,#7828,#7829,#7830,#7831,#7832,#7833,#7834,#7835,
#7836,#7837,#7838,#7839,#7840,#7841,#7842,#7843,#7844,#7845),(#7846,#7847,
#7848,#7849,#7850,#7851,#7852,#7853,#7854,#7855,#7856,#7857,#7858,#7859,
#7860,#7861,#7862,#7863,#7864,#7865,#7866,#7867,#7868,#7869,#7870,#7871,
#7872,#7873,#7874,#7875,#7876,#7877,#7878,#7879,#7880,#7881,#7882,#7883,
#7884),(#7885,#7886,#7887,#7888,#7889,#7890,#7891,#7892,#7893,#7894,#7895,
#7896,#7897,#7898,#7899,#7900,#7901,#7902,#7903,#7904,#7905,#7906,#7907,
#7908,#7909,#7910,#7911,#7912,#7913,#7914,#7915,#7916,#7917,#7918,#7919,
#7920,#7921,#7922,#7923),(#7924,#7925,#7926,#7927,#7928,#7929,#7930,#7931,
#7932,#7933,#7934,#7935,#7936,#7937,#7938,#7939,#7940,#7941,#7942,#7943,
#7944,#7945,#7946,#7947,#7948,#7949,#7950,#7951,#7952,#7953,#7954,#7955,
#7956,#7957,#7958,#7959,#7960,#7961,#7962)),.UNSPECIFIED.,.F.,.F.,.F.,(4,
4),(4,1,1,1,1,1,1,1,1,1,1,1,1,1,1,1,1,1,1,1,1,1,1,1,1,1,1,1,1,1,1,1,1,1,
1,1,4),(0.,0.0262983047615875),(11.6163931973415,12.6161795442943,13.6159658912471,
14.6157522381999,15.6155385851527,16.6153249321056,17.6151112790584,18.6148976260112,
19.614683972964,20.6144703199168,21.6142566668696,22.6140430138224,23.6138293607753,
24.6136157077281,25.6134020546809,26.6131884016337,27.6129747485865,28.6127610955393,
29.6125474424921,30.6123337894449,31.6121201363978,32.6119064833506,33.6116928303034,
34.6114791772562,35.611265524209,36.6110518711618,37.6108382181146,38.6106245650675,
39.6104109120203,40.6101972589731,41.6099836059259,42.6097699528787,43.6095562998315,
44.6093426467843,45.6091289937371,46.60891534069,47.6087016876428),
 .UNSPECIFIED.);
#102=B_SPLINE_CURVE_WITH_KNOTS('',3,(#6930,#6931,#6932,#6933,#6934,#6935,
#6936,#6937,#6938,#6939),.UNSPECIFIED.,.F.,.F.,(4,3,3,4),(-4.09157007060746,
-3.99914538781125,-2.99935904085844,-2.06546402602172),.UNSPECIFIED.);
#103=B_SPLINE_CURVE_WITH_KNOTS('',3,(#6942,#6943,#6944,#6945,#6946,#6947,
#6948),.UNSPECIFIED.,.F.,.F.,(4,3,4),(0.,0.999786346952812,1.11548660900404),
 .UNSPECIFIED.);
#104=B_SPLINE_CURVE_WITH_KNOTS('',3,(#6953,#6954,#6955,#6956,#6957,#6958,
#6959,#6960,#6961,#6962,#6963,#6964,#6965,#6966,#6967,#6968,#6969,#6970,
#6971,#6972,#6973,#6974),.UNSPECIFIED.,.F.,.F.,(4,3,3,3,3,3,3,4),(-10.3747553777871,
-9.99786346952814,-8.99807712257532,-7.99829077562251,-6.99850442866969,
-5.99871808171688,-4.99893173476407,-4.09157007060746),.UNSPECIFIED.);
#105=B_SPLINE_CURVE_WITH_KNOTS('',3,(#6975,#6976,#6977,#6978,#6979,#6980,
#6981,#6982,#6983,#6984,#6985,#6986,#6987,#6988,#6989,#6990,#6991,#6992,
#6993,#6994,#6995,#6996),.UNSPECIFIED.,.F.,.F.,(4,3,3,3,3,3,3,4),(1.11548660900404,
1.99957269390563,2.99935904085844,3.99914538781125,4.99893173476407,5.99871808171688,
6.99850442866969,7.39867191618363),.UNSPECIFIED.);
#106=B_SPLINE_CURVE_WITH_KNOTS('',3,(#7001,#7002,#7003,#7004,#7005,#7006,
#7007,#7008,#7009,#7010,#7011,#7012,#7013,#7014,#7015,#7016,#7017,#7018,
#7019,#7020,#7021,#7022),.UNSPECIFIED.,.F.,.F.,(4,3,3,3,3,3,3,4),(-16.6579406849666,
-15.996581551245,-14.9967952042922,-13.9970088573394,-12.9972225103866,
-11.9974361634338,-10.9976498164809,-10.3747553777871),.UNSPECIFIED.);
#107=B_SPLINE_CURVE_WITH_KNOTS('',3,(#7023,#7024,#7025,#7026,#7027,#7028,
#7029,#7030,#7031,#7032,#7033,#7034,#7035,#7036,#7037,#7038,#7039,#7040,
#7041,#7042,#7043,#7044),.UNSPECIFIED.,.F.,.F.,(4,3,3,3,3,3,3,4),(7.39867191618363,
7.99829077562251,8.99807712257532,9.99786346952813,10.9976498164809,11.9974361634338,
12.9972225103866,13.6818572233632),.UNSPECIFIED.);
#108=B_SPLINE_CURVE_WITH_KNOTS('',3,(#7049,#7050,#7051,#7052,#7053,#7054,
#7055,#7056,#7057,#7058,#7059,#7060,#7061,#7062,#7063,#7064,#7065,#7066,
#7067,#7068,#7069,#7070),.UNSPECIFIED.,.F.,.F.,(4,3,3,3,3,3,3,4),(-22.9411259921462,
-21.9952996329619,-20.9955132860091,-19.9957269390563,-18.9959405921035,
-17.9961542451506,-16.9963678981978,-16.6579406849666),.UNSPECIFIED.);
#109=B_SPLINE_CURVE_WITH_KNOTS('',3,(#7071,#7072,#7073,#7074,#7075,#7076,
#7077,#7078,#7079,#7080,#7081,#7082,#7083,#7084,#7085,#7086,#7087,#7088,
#7089,#7090,#7091,#7092),.UNSPECIFIED.,.F.,.F.,(4,3,3,3,3,3,3,4),(13.6818572233632,
13.9970088573394,14.9967952042922,15.996581551245,16.9963678981978,17.9961542451506,
18.9959405921034,19.9650425305428),.UNSPECIFIED.);
#110=B_SPLINE_CURVE_WITH_KNOTS('',3,(#7097,#7098,#7099,#7100,#7101,#7102,
#7103,#7104,#7105,#7106,#7107,#7108,#7109,#7110,#7111,#7112,#7113,#7114,
#7115,#7116,#7117,#7118,#7119,#7120,#7121),.UNSPECIFIED.,.F.,.F.,(4,3,3,
3,3,3,3,3,4),(-29.2243112993258,-28.9938040616316,-27.9940177146788,-26.994231367726,
-25.9944450207731,-24.9946586738203,-23.9948723268675,-22.9950859799147,
-22.9411259921462),.UNSPECIFIED.);
#111=B_SPLINE_CURVE_WITH_KNOTS('',3,(#7122,#7123,#7124,#7125,#7126,#7127,
#7128,#7129,#7130,#7131,#7132,#7133,#7134,#7135,#7136,#7137,#7138,#7139,
#7140,#7141,#7142,#7143,#7144,#7145,#7146),.UNSPECIFIED.,.F.,.F.,(4,3,3,
3,3,3,3,3,4),(19.9650425305428,19.9957269390563,20.9955132860091,21.9952996329619,
22.9950859799147,23.9948723268675,24.9946586738203,25.9944450207731,26.2482278377224),
 .UNSPECIFIED.);
#112=B_SPLINE_CURVE_WITH_KNOTS('',3,(#7151,#7152,#7153,#7154,#7155,#7156,
#7157,#7158,#7159,#7160,#7161,#7162,#7163,#7164,#7165,#7166,#7167,#7168,
#7169,#7170,#7171,#7172),.UNSPECIFIED.,.F.,.F.,(4,3,3,3,3,3,3,4),(-35.5074966065054,
-34.9925221433485,-33.9927357963956,-32.9929494494428,-31.99316310249,-30.9933767555372,
-29.9935904085844,-29.2243112993258),.UNSPECIFIED.);
#113=B_SPLINE_CURVE_WITH_KNOTS('',3,(#7173,#7174,#7175,#7176,#7177,#7178,
#7179,#7180,#7181,#7182,#7183,#7184,#7185,#7186,#7187,#7188,#7189,#7190,
#7191,#7192,#7193,#7194),.UNSPECIFIED.,.F.,.F.,(4,3,3,3,3,3,3,4),(26.2482278377224,
26.994231367726,27.9940177146788,28.9938040616316,29.9935904085844,30.9933767555372,
31.99316310249,32.531413144902),.UNSPECIFIED.);
#114=B_SPLINE_CURVE_WITH_KNOTS('',3,(#7200,#7201,#7202,#7203,#7204,#7205,
#7206,#7207),.UNSPECIFIED.,.F.,.F.,(4,1,1,1,1,4),(40.8407044966673,41.6099836059259,
42.6097699528787,43.6095562998315,44.6093426467843,45.5432376616211),
 .UNSPECIFIED.);
#115=B_SPLINE_CURVE_WITH_KNOTS('',3,(#7210,#7211,#7212,#7213,#7214,#7215,
#7216),.UNSPECIFIED.,.F.,.F.,(4,1,1,1,4),(40.8407044966673,41.3022408012082,
42.302027148161,43.3018134951138,44.3015998420666),.UNSPECIFIED.);
#116=B_SPLINE_CURVE_WITH_KNOTS('',3,(#7221,#7222,#7223,#7224,#7225,#7226,
#7227,#7228,#7229,#7230,#7231),.UNSPECIFIED.,.F.,.F.,(4,1,1,1,1,1,1,1,4),
(34.5575191894877,34.6114791772562,35.611265524209,36.6110518711618,37.6108382181146,
38.6106245650675,39.6104109120203,40.6101972589731,40.8407044966673),
 .UNSPECIFIED.);
#117=B_SPLINE_CURVE_WITH_KNOTS('',3,(#7232,#7233,#7234,#7235,#7236,#7237,
#7238,#7239,#7240,#7241),.UNSPECIFIED.,.F.,.F.,(4,1,1,1,1,1,1,4),(34.5575191894877,
35.3035227194913,36.3033090664441,37.3030954133969,38.3028817603497,39.3026681073025,
40.3024544542553,40.8407044966673),.UNSPECIFIED.);
#118=B_SPLINE_CURVE_WITH_KNOTS('',3,(#7246,#7247,#7248,#7249,#7250,#7251,
#7252,#7253,#7254,#7255),.UNSPECIFIED.,.F.,.F.,(4,1,1,1,1,1,1,4),(28.2743338823081,
28.6127610955393,29.6125474424921,30.6123337894449,31.6121201363978,32.6119064833506,
33.6116928303034,34.5575191894877),.UNSPECIFIED.);
#119=B_SPLINE_CURVE_WITH_KNOTS('',3,(#7256,#7257,#7258,#7259,#7260,#7261,
#7262,#7263,#7264,#7265,#7266),.UNSPECIFIED.,.F.,.F.,(4,1,1,1,1,1,1,1,4),
(28.2743338823081,28.3050182908216,29.3048046377744,30.3045909847272,31.30437733168,
32.3041636786328,33.3039500255856,34.3037363725385,34.5575191894877),
 .UNSPECIFIED.);
#120=B_SPLINE_CURVE_WITH_KNOTS('',3,(#7271,#7272,#7273,#7274,#7275,#7276,
#7277,#7278,#7279,#7280),.UNSPECIFIED.,.F.,.F.,(4,1,1,1,1,1,1,4),(21.9911485751285,
22.6140430138224,23.6138293607753,24.6136157077281,25.6134020546809,26.6131884016337,
27.6129747485865,28.2743338823081),.UNSPECIFIED.);
#121=B_SPLINE_CURVE_WITH_KNOTS('',3,(#7281,#7282,#7283,#7284,#7285,#7286,
#7287,#7288,#7289,#7290),.UNSPECIFIED.,.F.,.F.,(4,1,1,1,1,1,1,4),(21.9911485751285,
22.3063002091047,23.3060865560575,24.3058729030103,25.3056592499631,26.305445596916,
27.3052319438688,28.2743338823081),.UNSPECIFIED.);
#122=B_SPLINE_CURVE_WITH_KNOTS('',3,(#7295,#7296,#7297,#7298,#7299,#7300,
#7301,#7302,#7303,#7304),.UNSPECIFIED.,.F.,.F.,(4,1,1,1,1,1,1,4),(15.707963267949,
16.6153249321056,17.6151112790584,18.6148976260112,19.614683972964,20.6144703199168,
21.6142566668696,21.9911485751285),.UNSPECIFIED.);
#123=B_SPLINE_CURVE_WITH_KNOTS('',3,(#7305,#7306,#7307,#7308,#7309,#7310,
#7311,#7312,#7313,#7314),.UNSPECIFIED.,.F.,.F.,(4,1,1,1,1,1,1,4),(15.707963267949,
16.3075821273878,17.3073684743406,18.3071548212935,19.3069411682463,20.3067275151991,
21.3065138621519,21.9911485751285),.UNSPECIFIED.);
#124=B_SPLINE_CURVE_WITH_KNOTS('',3,(#7317,#7318,#7319,#7320,#7321,#7322,
#7323,#7324,#7325,#7326,#7327,#7328,#7329,#7330,#7331,#7332,#7333,#7334,
#7335,#7336,#7337,#7338,#7339,#7340,#7341,#7342,#7343,#7344,#7345,#7346,
#7347,#7348,#7349,#7350,#7351,#7352,#7353,#7354,#7355,#7356,#7357,#7358,
#7359,#7360,#7361,#7362,#7363,#7364,#7365,#7366,#7367,#7368,#7369,#7370,
#7371,#7372,#7373,#7374,#7375,#7376,#7377,#7378,#7379,#7380,#7381,#7382,
#7383,#7384,#7385,#7386,#7387,#7388,#7389,#7390,#7391,#7392),
 .UNSPECIFIED.,.F.,.F.,(4,3,3,3,3,3,3,3,3,3,3,3,3,3,3,3,3,3,3,3,3,3,3,3,
3,4),(-0.178587760439504,-0.17361180774909,-0.163438350924944,-0.158375688276003,
-0.155636584119497,-0.144832458277613,-0.140259732391418,-0.137183188509201,
-0.134746510299358,-0.123387595779259,-0.111954473335422,-0.106069923958762,
-0.103723902609418,-0.0922241531559208,-0.0806961340114307,-0.0752220429825342,
-0.0719210107775354,-0.0694880548095068,-0.0575218446312738,-0.045279006273988,
-0.0393960404635036,-0.0368040337146181,-0.0343328896694744,-0.0216376030695688,
-0.00903059604707899,0.),.UNSPECIFIED.);
#125=B_SPLINE_CURVE_WITH_KNOTS('',3,(#7397,#7398,#7399,#7400,#7401,#7402,
#7403,#7404,#7405,#7406,#7407,#7408,#7409,#7410,#7411,#7412,#7413,#7414,
#7415,#7416,#7417,#7418,#7419,#7420,#7421,#7422,#7423,#7424,#7425,#7426,
#7427,#7428,#7429,#7430,#7431,#7432,#7433,#7434,#7435,#7436,#7437,#7438,
#7439,#7440,#7441,#7442,#7443,#7444,#7445,#7446,#7447,#7448,#7449,#7450,
#7451,#7452,#7453,#7454,#7455,#7456,#7457,#7458,#7459,#7460,#7461,#7462,
#7463,#7464,#7465,#7466,#7467,#7468,#7469),.UNSPECIFIED.,.F.,.F.,(4,3,3,
3,3,3,3,3,3,3,3,3,3,3,3,3,3,3,3,3,3,3,3,3,4),(-0.177567088092164,-0.171205860781276,
-0.159841364771409,-0.153341448629585,-0.149825019995913,-0.137364180358316,
-0.13022989440132,-0.127506551868041,-0.125034870535725,-0.113089167658055,
-0.101422640254504,-0.0960446801741604,-0.0933155330928928,-0.091156106491866,
-0.0802898927023465,-0.0702536561145532,-0.0605144873326988,-0.0580925158103782,
-0.0469016452609415,-0.0358502799243893,-0.0306242181708044,-0.0277817060826135,
-0.0171983362218047,-0.00699990470760896,0.),.UNSPECIFIED.);
#126=B_SPLINE_CURVE_WITH_KNOTS('',3,(#7626,#7627,#7628,#7629,#7630,#7631,
#7632),.UNSPECIFIED.,.F.,.F.,(4,3,4),(32.531413144902,32.9929494494428,
33.9268444642796),.UNSPECIFIED.);
#127=B_SPLINE_CURVE_WITH_KNOTS('',3,(#7634,#7635,#7636,#7637,#7638,#7639,
#7640,#7641,#7642,#7643,#7644,#7645,#7646,#7647,#7648,#7649,#7650,#7651,
#7652,#7653,#7654,#7655,#7656,#7657,#7658,#7659,#7660,#7661,#7662,#7663,
#7664,#7665,#7666,#7667,#7668,#7669,#7670,#7671,#7672,#7673,#7674,#7675,
#7676,#7677,#7678,#7679,#7680,#7681,#7682,#7683,#7684,#7685,#7686,#7687,
#7688,#7689,#7690,#7691,#7692,#7693,#7694,#7695,#7696,#7697,#7698,#7699,
#7700,#7701,#7702,#7703,#7704,#7705,#7706,#7707,#7708,#7709),
 .UNSPECIFIED.,.F.,.F.,(4,3,3,3,3,3,3,3,3,3,3,3,3,3,3,3,3,3,3,3,3,3,3,3,
3,4),(-0.178587760439503,-0.173611807749089,-0.163438350924943,-0.158375685688331,
-0.155636582785503,-0.144832452490873,-0.140259718887796,-0.137183155499747,
-0.134746503227007,-0.12338758703633,-0.111954465066202,-0.106069912314992,
-0.103723896170116,-0.0922241531559212,-0.0806961340114311,-0.0752220431672022,
-0.0719210138736596,-0.0694880559864147,-0.0575218436472125,-0.0452790030681591,
-0.0393960367230259,-0.0368040370944524,-0.0343328909447597,-0.0216376025540469,
-0.00903060057598744,0.),.UNSPECIFIED.);
#128=B_SPLINE_CURVE_WITH_KNOTS('',3,(#7710,#7711,#7712,#7713,#7714,#7715,
#7716,#7717,#7718),.UNSPECIFIED.,.F.,.F.,(4,1,1,1,1,1,4),(10.374755377787,
11.3086503926238,12.3084367395766,13.3082230865294,14.3080094334822,15.307795780435,
15.707963267949),.UNSPECIFIED.);
#129=B_SPLINE_CURVE_WITH_KNOTS('',3,(#7724,#7725,#7726,#7727,#7728,#7729,
#7730,#7731,#7732,#7733,#7734,#7735,#7736,#7737,#7738,#7739,#7740,#7741,
#7742,#7743,#7744,#7745,#7746,#7747,#7748,#7749,#7750,#7751,#7752,#7753,
#7754,#7755,#7756,#7757,#7758,#7759,#7760,#7761,#7762,#7763,#7764,#7765,
#7766,#7767,#7768,#7769,#7770,#7771,#7772,#7773,#7774,#7775,#7776,#7777,
#7778,#7779,#7780,#7781,#7782,#7783,#7784,#7785,#7786,#7787,#7788,#7789,
#7790,#7791,#7792,#7793,#7794,#7795,#7796),.UNSPECIFIED.,.F.,.F.,(4,3,3,
3,3,3,3,3,3,3,3,3,3,3,3,3,3,3,3,3,3,3,3,3,4),(-0.177567088092158,-0.171205860781269,
-0.159841364771403,-0.153341449957138,-0.149825021408317,-0.137364182301213,
-0.130229896101354,-0.127506561096828,-0.125034891677152,-0.113089191744828,
-0.101422670425347,-0.0960447146844191,-0.0933157066615757,-0.0911564534648362,
-0.0802898927023405,-0.0702536561145479,-0.0605144868244642,-0.0580925152771776,
-0.0469016447884122,-0.0358502738466785,-0.0306242089636902,-0.0277817043216266,
-0.0171983284784898,-0.00699988795734099,0.),.UNSPECIFIED.);
#130=B_SPLINE_CURVE_WITH_KNOTS('',3,(#7799,#7800,#7801,#7802,#7803,#7804,
#7805,#7806),.UNSPECIFIED.,.F.,.F.,(4,1,1,1,1,4),(11.6163931973415,12.6161795442943,
13.6159658912471,14.6157522381999,15.6155385851527,15.707963267949),
 .UNSPECIFIED.);
#131=B_SPLINE_CURVE_WITH_KNOTS('',3,(#7963,#7964,#7965,#7966),
 .UNSPECIFIED.,.F.,.F.,(4,4),(-35.9923084903013,-35.5074966065054),
 .UNSPECIFIED.);
#241=SHAPE_REPRESENTATION_RELATIONSHIP('SRR','None',#11484,#253);
#253=ADVANCED_BREP_SHAPE_REPRESENTATION('',(#277),#11423);
#265=STYLED_ITEM('',(#11616),#277);
#277=MANIFOLD_SOLID_BREP('Body1',#4466);
#306=FACE_BOUND('',#944,.T.);
#369=PLANE('',#4820);
#370=PLANE('',#4823);
#371=PLANE('',#4828);
#372=PLANE('',#4829);
#373=PLANE('',#4830);
#374=PLANE('',#4831);
#375=PLANE('',#4832);
#376=PLANE('',#4833);
#377=PLANE('',#4834);
#378=PLANE('',#4835);
#379=PLANE('',#4842);
#456=CYLINDRICAL_SURFACE('',#4807,0.96675);
#457=CYLINDRICAL_SURFACE('',#4809,0.96675);
#458=CYLINDRICAL_SURFACE('',#4810,0.96675);
#459=CYLINDRICAL_SURFACE('',#4811,0.96675);
#460=CYLINDRICAL_SURFACE('',#4812,0.96675);
#461=CYLINDRICAL_SURFACE('',#4813,0.96675);
#462=CYLINDRICAL_SURFACE('',#4814,0.739);
#463=CYLINDRICAL_SURFACE('',#4816,0.739);
#464=CYLINDRICAL_SURFACE('',#4817,0.739);
#465=CYLINDRICAL_SURFACE('',#4818,0.739);
#466=CYLINDRICAL_SURFACE('',#4819,0.739);
#467=CYLINDRICAL_SURFACE('',#4827,0.739);
#468=CYLINDRICAL_SURFACE('',#4838,0.96675);
#630=FACE_OUTER_BOUND('',#920,.T.);
#631=FACE_OUTER_BOUND('',#921,.T.);
#632=FACE_OUTER_BOUND('',#922,.T.);
#633=FACE_OUTER_BOUND('',#923,.T.);
#634=FACE_OUTER_BOUND('',#924,.T.);
#635=FACE_OUTER_BOUND('',#925,.T.);
#636=FACE_OUTER_BOUND('',#926,.T.);
#637=FACE_OUTER_BOUND('',#927,.T.);
#638=FACE_OUTER_BOUND('',#928,.T.);
#639=FACE_OUTER_BOUND('',#929,.T.);
#640=FACE_OUTER_BOUND('',#930,.T.);
#641=FACE_OUTER_BOUND('',#931,.T.);
#642=FACE_OUTER_BOUND('',#932,.T.);
#643=FACE_OUTER_BOUND('',#933,.T.);
#644=FACE_OUTER_BOUND('',#934,.T.);
#645=FACE_OUTER_BOUND('',#935,.T.);
#646=FACE_OUTER_BOUND('',#936,.T.);
#647=FACE_OUTER_BOUND('',#937,.T.);
#648=FACE_OUTER_BOUND('',#938,.T.);
#649=FACE_OUTER_BOUND('',#939,.T.);
#650=FACE_OUTER_BOUND('',#940,.T.);
#651=FACE_OUTER_BOUND('',#941,.T.);
#652=FACE_OUTER_BOUND('',#942,.T.);
#653=FACE_OUTER_BOUND('',#943,.T.);
#654=FACE_OUTER_BOUND('',#945,.T.);
#655=FACE_OUTER_BOUND('',#946,.T.);
#656=FACE_OUTER_BOUND('',#947,.T.);
#657=FACE_OUTER_BOUND('',#948,.T.);
#920=EDGE_LOOP('',(#3331,#3332,#3333,#3334));
#921=EDGE_LOOP('',(#3335,#3336,#3337,#3338));
#922=EDGE_LOOP('',(#3339,#3340,#3341,#3342));
#923=EDGE_LOOP('',(#3343,#3344,#3345,#3346));
#924=EDGE_LOOP('',(#3347,#3348,#3349,#3350));
#925=EDGE_LOOP('',(#3351,#3352,#3353,#3354));
#926=EDGE_LOOP('',(#3355,#3356,#3357,#3358));
#927=EDGE_LOOP('',(#3359,#3360,#3361,#3362));
#928=EDGE_LOOP('',(#3363,#3364,#3365,#3366));
#929=EDGE_LOOP('',(#3367,#3368,#3369,#3370));
#930=EDGE_LOOP('',(#3371,#3372,#3373,#3374));
#931=EDGE_LOOP('',(#3375,#3376,#3377,#3378,#3379));
#932=EDGE_LOOP('',(#3380,#3381,#3382,#3383,#3384,#3385,#3386,#3387,#3388,
#3389,#3390,#3391,#3392,#3393,#3394));
#933=EDGE_LOOP('',(#3395,#3396,#3397,#3398,#3399));
#934=EDGE_LOOP('',(#3400,#3401,#3402,#3403));
#935=EDGE_LOOP('',(#3404,#3405,#3406,#3407,#3408,#3409,#3410,#3411,#3412,
#3413,#3414,#3415,#3416,#3417,#3418));
#936=EDGE_LOOP('',(#3419,#3420,#3421,#3422));
#937=EDGE_LOOP('',(#3423,#3424,#3425,#3426));
#938=EDGE_LOOP('',(#3427,#3428,#3429,#3430));
#939=EDGE_LOOP('',(#3431,#3432,#3433,#3434));
#940=EDGE_LOOP('',(#3435,#3436,#3437,#3438));
#941=EDGE_LOOP('',(#3439,#3440,#3441,#3442));
#942=EDGE_LOOP('',(#3443,#3444,#3445,#3446,#3447,#3448));
#943=EDGE_LOOP('',(#3449));
#944=EDGE_LOOP('',(#3450,#3451,#3452,#3453,#3454,#3455));
#945=EDGE_LOOP('',(#3456,#3457,#3458,#3459,#3460,#3461));
#946=EDGE_LOOP('',(#3462,#3463,#3464,#3465));
#947=EDGE_LOOP('',(#3466,#3467,#3468,#3469,#3470,#3471));
#948=EDGE_LOOP('',(#3472));
#1202=LINE('',#6928,#1492);
#1203=LINE('',#6952,#1493);
#1204=LINE('',#7000,#1494);
#1205=LINE('',#7048,#1495);
#1206=LINE('',#7096,#1496);
#1207=LINE('',#7150,#1497);
#1208=LINE('',#7198,#1498);
#1209=LINE('',#7220,#1499);
#1210=LINE('',#7245,#1500);
#1211=LINE('',#7270,#1501);
#1212=LINE('',#7294,#1502);
#1213=LINE('',#7970,#1503);
#1214=LINE('',#7972,#1504);
#1215=LINE('',#7974,#1505);
#1216=LINE('',#7975,#1506);
#1217=LINE('',#7978,#1507);
#1218=LINE('',#7980,#1508);
#1219=LINE('',#7981,#1509);
#1220=LINE('',#7984,#1510);
#1221=LINE('',#7986,#1511);
#1222=LINE('',#7987,#1512);
#1223=LINE('',#7990,#1513);
#1224=LINE('',#7992,#1514);
#1225=LINE('',#7993,#1515);
#1226=LINE('',#7996,#1516);
#1227=LINE('',#7998,#1517);
#1228=LINE('',#7999,#1518);
#1229=LINE('',#8001,#1519);
#1230=LINE('',#8002,#1520);
#1231=LINE('',#8008,#1521);
#1232=LINE('',#8014,#1522);
#1492=VECTOR('',#5588,1.);
#1493=VECTOR('',#5593,1.);
#1494=VECTOR('',#5596,1.);
#1495=VECTOR('',#5599,1.);
#1496=VECTOR('',#5602,1.);
#1497=VECTOR('',#5605,1.);
#1498=VECTOR('',#5608,0.739);
#1499=VECTOR('',#5613,0.739);
#1500=VECTOR('',#5616,0.739);
#1501=VECTOR('',#5619,0.739);
#1502=VECTOR('',#5622,0.739);
#1503=VECTOR('',#5641,10.);
#1504=VECTOR('',#5642,10.);
#1505=VECTOR('',#5643,10.);
#1506=VECTOR('',#5644,10.);
#1507=VECTOR('',#5647,10.);
#1508=VECTOR('',#5648,10.);
#1509=VECTOR('',#5649,10.);
#1510=VECTOR('',#5652,10.);
#1511=VECTOR('',#5653,10.);
#1512=VECTOR('',#5654,10.);
#1513=VECTOR('',#5657,10.);
#1514=VECTOR('',#5658,10.);
#1515=VECTOR('',#5659,10.);
#1516=VECTOR('',#5662,10.);
#1517=VECTOR('',#5663,10.);
#1518=VECTOR('',#5664,10.);
#1519=VECTOR('',#5667,10.);
#1520=VECTOR('',#5668,10.);
#1521=VECTOR('',#5677,0.9);
#1522=VECTOR('',#5686,0.875);
#1771=CIRCLE('',#4808,0.96675);
#1772=CIRCLE('',#4815,0.739);
#1773=CIRCLE('',#4821,0.96675);
#1774=CIRCLE('',#4822,0.96675);
#1775=CIRCLE('',#4824,0.96675);
#1776=CIRCLE('',#4825,0.96675);
#1777=CIRCLE('',#4826,0.739);
#1778=CIRCLE('',#4836,0.8);
#1779=CIRCLE('',#4839,0.96675);
#1780=CIRCLE('',#4841,0.75);
#2001=VERTEX_POINT('',#6926);
#2002=VERTEX_POINT('',#6927);
#2003=VERTEX_POINT('',#6929);
#2004=VERTEX_POINT('',#6940);
#2005=VERTEX_POINT('',#6950);
#2006=VERTEX_POINT('',#6951);
#2007=VERTEX_POINT('',#6998);
#2008=VERTEX_POINT('',#6999);
#2009=VERTEX_POINT('',#7046);
#2010=VERTEX_POINT('',#7047);
#2011=VERTEX_POINT('',#7094);
#2012=VERTEX_POINT('',#7095);
#2013=VERTEX_POINT('',#7148);
#2014=VERTEX_POINT('',#7149);
#2015=VERTEX_POINT('',#7196);
#2016=VERTEX_POINT('',#7197);
#2017=VERTEX_POINT('',#7199);
#2018=VERTEX_POINT('',#7208);
#2019=VERTEX_POINT('',#7218);
#2020=VERTEX_POINT('',#7219);
#2021=VERTEX_POINT('',#7243);
#2022=VERTEX_POINT('',#7244);
#2023=VERTEX_POINT('',#7268);
#2024=VERTEX_POINT('',#7269);
#2025=VERTEX_POINT('',#7292);
#2026=VERTEX_POINT('',#7293);
#2027=VERTEX_POINT('',#7316);
#2028=VERTEX_POINT('',#7393);
#2029=VERTEX_POINT('',#7395);
#2030=VERTEX_POINT('',#7633);
#2031=VERTEX_POINT('',#7720);
#2032=VERTEX_POINT('',#7723);
#2033=VERTEX_POINT('',#7968);
#2034=VERTEX_POINT('',#7969);
#2035=VERTEX_POINT('',#7971);
#2036=VERTEX_POINT('',#7973);
#2037=VERTEX_POINT('',#7977);
#2038=VERTEX_POINT('',#7979);
#2039=VERTEX_POINT('',#7983);
#2040=VERTEX_POINT('',#7985);
#2041=VERTEX_POINT('',#7989);
#2042=VERTEX_POINT('',#7991);
#2043=VERTEX_POINT('',#7995);
#2044=VERTEX_POINT('',#7997);
#2045=VERTEX_POINT('',#8005);
#2046=VERTEX_POINT('',#8012);
#2483=EDGE_CURVE('',#2001,#2002,#1202,.T.);
#2484=EDGE_CURVE('',#2001,#2003,#102,.T.);
#2485=EDGE_CURVE('',#2003,#2004,#1771,.T.);
#2486=EDGE_CURVE('',#2004,#2002,#103,.T.);
#2487=EDGE_CURVE('',#2005,#2006,#1203,.T.);
#2488=EDGE_CURVE('',#2005,#2001,#104,.T.);
#2489=EDGE_CURVE('',#2002,#2006,#105,.T.);
#2490=EDGE_CURVE('',#2007,#2008,#1204,.T.);
#2491=EDGE_CURVE('',#2007,#2005,#106,.T.);
#2492=EDGE_CURVE('',#2006,#2008,#107,.T.);
#2493=EDGE_CURVE('',#2009,#2010,#1205,.T.);
#2494=EDGE_CURVE('',#2009,#2007,#108,.T.);
#2495=EDGE_CURVE('',#2008,#2010,#109,.T.);
#2496=EDGE_CURVE('',#2011,#2012,#1206,.T.);
#2497=EDGE_CURVE('',#2011,#2009,#110,.T.);
#2498=EDGE_CURVE('',#2010,#2012,#111,.T.);
#2499=EDGE_CURVE('',#2013,#2014,#1207,.T.);
#2500=EDGE_CURVE('',#2013,#2011,#112,.T.);
#2501=EDGE_CURVE('',#2012,#2014,#113,.T.);
#2502=EDGE_CURVE('',#2015,#2016,#1208,.T.);
#2503=EDGE_CURVE('',#2015,#2017,#114,.T.);
#2504=EDGE_CURVE('',#2018,#2017,#1772,.T.);
#2505=EDGE_CURVE('',#2016,#2018,#115,.T.);
#2506=EDGE_CURVE('',#2019,#2020,#1209,.T.);
#2507=EDGE_CURVE('',#2019,#2015,#116,.T.);
#2508=EDGE_CURVE('',#2020,#2016,#117,.T.);
#2509=EDGE_CURVE('',#2021,#2022,#1210,.T.);
#2510=EDGE_CURVE('',#2021,#2019,#118,.T.);
#2511=EDGE_CURVE('',#2022,#2020,#119,.T.);
#2512=EDGE_CURVE('',#2023,#2024,#1211,.T.);
#2513=EDGE_CURVE('',#2023,#2021,#120,.T.);
#2514=EDGE_CURVE('',#2024,#2022,#121,.T.);
#2515=EDGE_CURVE('',#2025,#2026,#1212,.T.);
#2516=EDGE_CURVE('',#2025,#2023,#122,.T.);
#2517=EDGE_CURVE('',#2026,#2024,#123,.T.);
#2518=EDGE_CURVE('',#2017,#2027,#124,.T.);
#2519=EDGE_CURVE('',#2028,#2027,#1773,.F.);
#2520=EDGE_CURVE('',#2029,#2028,#1774,.F.);
#2521=EDGE_CURVE('',#2029,#2018,#125,.T.);
#2522=EDGE_CURVE('',#2014,#2029,#126,.T.);
#2523=EDGE_CURVE('',#2030,#2004,#127,.T.);
#2524=EDGE_CURVE('',#2030,#2026,#128,.T.);
#2525=EDGE_CURVE('',#2004,#2031,#1775,.T.);
#2526=EDGE_CURVE('',#2031,#2003,#1776,.T.);
#2527=EDGE_CURVE('',#2003,#2032,#129,.T.);
#2528=EDGE_CURVE('',#2032,#2030,#1777,.T.);
#2529=EDGE_CURVE('',#2032,#2025,#130,.T.);
#2530=EDGE_CURVE('',#2027,#2013,#131,.T.);
#2531=EDGE_CURVE('',#2033,#2034,#1213,.T.);
#2532=EDGE_CURVE('',#2033,#2035,#1214,.T.);
#2533=EDGE_CURVE('',#2035,#2036,#1215,.T.);
#2534=EDGE_CURVE('',#2034,#2036,#1216,.T.);
#2535=EDGE_CURVE('',#2037,#2033,#1217,.T.);
#2536=EDGE_CURVE('',#2037,#2038,#1218,.T.);
#2537=EDGE_CURVE('',#2038,#2035,#1219,.T.);
#2538=EDGE_CURVE('',#2039,#2037,#1220,.T.);
#2539=EDGE_CURVE('',#2039,#2040,#1221,.T.);
#2540=EDGE_CURVE('',#2040,#2038,#1222,.T.);
#2541=EDGE_CURVE('',#2041,#2039,#1223,.T.);
#2542=EDGE_CURVE('',#2041,#2042,#1224,.T.);
#2543=EDGE_CURVE('',#2042,#2040,#1225,.T.);
#2544=EDGE_CURVE('',#2043,#2041,#1226,.T.);
#2545=EDGE_CURVE('',#2043,#2044,#1227,.T.);
#2546=EDGE_CURVE('',#2044,#2042,#1228,.T.);
#2547=EDGE_CURVE('',#2034,#2043,#1229,.T.);
#2548=EDGE_CURVE('',#2036,#2044,#1230,.T.);
#2549=EDGE_CURVE('',#2045,#2045,#1778,.T.);
#2550=EDGE_CURVE('',#2031,#2045,#1231,.T.);
#2551=EDGE_CURVE('',#2027,#2029,#1779,.F.);
#2552=EDGE_CURVE('',#2046,#2046,#1780,.T.);
#2553=EDGE_CURVE('',#2046,#2028,#1232,.T.);
#3331=ORIENTED_EDGE('',*,*,#2483,.F.);
#3332=ORIENTED_EDGE('',*,*,#2484,.T.);
#3333=ORIENTED_EDGE('',*,*,#2485,.T.);
#3334=ORIENTED_EDGE('',*,*,#2486,.T.);
#3335=ORIENTED_EDGE('',*,*,#2487,.F.);
#3336=ORIENTED_EDGE('',*,*,#2488,.T.);
#3337=ORIENTED_EDGE('',*,*,#2483,.T.);
#3338=ORIENTED_EDGE('',*,*,#2489,.T.);
#3339=ORIENTED_EDGE('',*,*,#2490,.F.);
#3340=ORIENTED_EDGE('',*,*,#2491,.T.);
#3341=ORIENTED_EDGE('',*,*,#2487,.T.);
#3342=ORIENTED_EDGE('',*,*,#2492,.T.);
#3343=ORIENTED_EDGE('',*,*,#2493,.F.);
#3344=ORIENTED_EDGE('',*,*,#2494,.T.);
#3345=ORIENTED_EDGE('',*,*,#2490,.T.);
#3346=ORIENTED_EDGE('',*,*,#2495,.T.);
#3347=ORIENTED_EDGE('',*,*,#2496,.F.);
#3348=ORIENTED_EDGE('',*,*,#2497,.T.);
#3349=ORIENTED_EDGE('',*,*,#2493,.T.);
#3350=ORIENTED_EDGE('',*,*,#2498,.T.);
#3351=ORIENTED_EDGE('',*,*,#2499,.F.);
#3352=ORIENTED_EDGE('',*,*,#2500,.T.);
#3353=ORIENTED_EDGE('',*,*,#2496,.T.);
#3354=ORIENTED_EDGE('',*,*,#2501,.T.);
#3355=ORIENTED_EDGE('',*,*,#2502,.F.);
#3356=ORIENTED_EDGE('',*,*,#2503,.T.);
#3357=ORIENTED_EDGE('',*,*,#2504,.F.);
#3358=ORIENTED_EDGE('',*,*,#2505,.F.);
#3359=ORIENTED_EDGE('',*,*,#2506,.F.);
#3360=ORIENTED_EDGE('',*,*,#2507,.T.);
#3361=ORIENTED_EDGE('',*,*,#2502,.T.);
#3362=ORIENTED_EDGE('',*,*,#2508,.F.);
#3363=ORIENTED_EDGE('',*,*,#2509,.F.);
#3364=ORIENTED_EDGE('',*,*,#2510,.T.);
#3365=ORIENTED_EDGE('',*,*,#2506,.T.);
#3366=ORIENTED_EDGE('',*,*,#2511,.F.);
#3367=ORIENTED_EDGE('',*,*,#2512,.F.);
#3368=ORIENTED_EDGE('',*,*,#2513,.T.);
#3369=ORIENTED_EDGE('',*,*,#2509,.T.);
#3370=ORIENTED_EDGE('',*,*,#2514,.F.);
#3371=ORIENTED_EDGE('',*,*,#2515,.F.);
#3372=ORIENTED_EDGE('',*,*,#2516,.T.);
#3373=ORIENTED_EDGE('',*,*,#2512,.T.);
#3374=ORIENTED_EDGE('',*,*,#2517,.F.);
#3375=ORIENTED_EDGE('',*,*,#2504,.T.);
#3376=ORIENTED_EDGE('',*,*,#2518,.T.);
#3377=ORIENTED_EDGE('',*,*,#2519,.F.);
#3378=ORIENTED_EDGE('',*,*,#2520,.F.);
#3379=ORIENTED_EDGE('',*,*,#2521,.T.);
#3380=ORIENTED_EDGE('',*,*,#2521,.F.);
#3381=ORIENTED_EDGE('',*,*,#2522,.F.);
#3382=ORIENTED_EDGE('',*,*,#2501,.F.);
#3383=ORIENTED_EDGE('',*,*,#2498,.F.);
#3384=ORIENTED_EDGE('',*,*,#2495,.F.);
#3385=ORIENTED_EDGE('',*,*,#2492,.F.);
#3386=ORIENTED_EDGE('',*,*,#2489,.F.);
#3387=ORIENTED_EDGE('',*,*,#2486,.F.);
#3388=ORIENTED_EDGE('',*,*,#2523,.F.);
#3389=ORIENTED_EDGE('',*,*,#2524,.T.);
#3390=ORIENTED_EDGE('',*,*,#2517,.T.);
#3391=ORIENTED_EDGE('',*,*,#2514,.T.);
#3392=ORIENTED_EDGE('',*,*,#2511,.T.);
#3393=ORIENTED_EDGE('',*,*,#2508,.T.);
#3394=ORIENTED_EDGE('',*,*,#2505,.T.);
#3395=ORIENTED_EDGE('',*,*,#2525,.T.);
#3396=ORIENTED_EDGE('',*,*,#2526,.T.);
#3397=ORIENTED_EDGE('',*,*,#2527,.T.);
#3398=ORIENTED_EDGE('',*,*,#2528,.T.);
#3399=ORIENTED_EDGE('',*,*,#2523,.T.);
#3400=ORIENTED_EDGE('',*,*,#2515,.T.);
#3401=ORIENTED_EDGE('',*,*,#2524,.F.);
#3402=ORIENTED_EDGE('',*,*,#2528,.F.);
#3403=ORIENTED_EDGE('',*,*,#2529,.T.);
#3404=ORIENTED_EDGE('',*,*,#2518,.F.);
#3405=ORIENTED_EDGE('',*,*,#2503,.F.);
#3406=ORIENTED_EDGE('',*,*,#2507,.F.);
#3407=ORIENTED_EDGE('',*,*,#2510,.F.);
#3408=ORIENTED_EDGE('',*,*,#2513,.F.);
#3409=ORIENTED_EDGE('',*,*,#2516,.F.);
#3410=ORIENTED_EDGE('',*,*,#2529,.F.);
#3411=ORIENTED_EDGE('',*,*,#2527,.F.);
#3412=ORIENTED_EDGE('',*,*,#2484,.F.);
#3413=ORIENTED_EDGE('',*,*,#2488,.F.);
#3414=ORIENTED_EDGE('',*,*,#2491,.F.);
#3415=ORIENTED_EDGE('',*,*,#2494,.F.);
#3416=ORIENTED_EDGE('',*,*,#2497,.F.);
#3417=ORIENTED_EDGE('',*,*,#2500,.F.);
#3418=ORIENTED_EDGE('',*,*,#2530,.F.);
#3419=ORIENTED_EDGE('',*,*,#2531,.F.);
#3420=ORIENTED_EDGE('',*,*,#2532,.T.);
#3421=ORIENTED_EDGE('',*,*,#2533,.T.);
#3422=ORIENTED_EDGE('',*,*,#2534,.F.);
#3423=ORIENTED_EDGE('',*,*,#2535,.F.);
#3424=ORIENTED_EDGE('',*,*,#2536,.T.);
#3425=ORIENTED_EDGE('',*,*,#2537,.T.);
#3426=ORIENTED_EDGE('',*,*,#2532,.F.);
#3427=ORIENTED_EDGE('',*,*,#2538,.F.);
#3428=ORIENTED_EDGE('',*,*,#2539,.T.);
#3429=ORIENTED_EDGE('',*,*,#2540,.T.);
#3430=ORIENTED_EDGE('',*,*,#2536,.F.);
#3431=ORIENTED_EDGE('',*,*,#2541,.F.);
#3432=ORIENTED_EDGE('',*,*,#2542,.T.);
#3433=ORIENTED_EDGE('',*,*,#2543,.T.);
#3434=ORIENTED_EDGE('',*,*,#2539,.F.);
#3435=ORIENTED_EDGE('',*,*,#2544,.F.);
#3436=ORIENTED_EDGE('',*,*,#2545,.T.);
#3437=ORIENTED_EDGE('',*,*,#2546,.T.);
#3438=ORIENTED_EDGE('',*,*,#2542,.F.);
#3439=ORIENTED_EDGE('',*,*,#2547,.F.);
#3440=ORIENTED_EDGE('',*,*,#2534,.T.);
#3441=ORIENTED_EDGE('',*,*,#2548,.T.);
#3442=ORIENTED_EDGE('',*,*,#2545,.F.);
#3443=ORIENTED_EDGE('',*,*,#2548,.F.);
#3444=ORIENTED_EDGE('',*,*,#2533,.F.);
#3445=ORIENTED_EDGE('',*,*,#2537,.F.);
#3446=ORIENTED_EDGE('',*,*,#2540,.F.);
#3447=ORIENTED_EDGE('',*,*,#2543,.F.);
#3448=ORIENTED_EDGE('',*,*,#2546,.F.);
#3449=ORIENTED_EDGE('',*,*,#2549,.F.);
#3450=ORIENTED_EDGE('',*,*,#2531,.T.);
#3451=ORIENTED_EDGE('',*,*,#2547,.T.);
#3452=ORIENTED_EDGE('',*,*,#2544,.T.);
#3453=ORIENTED_EDGE('',*,*,#2541,.T.);
#3454=ORIENTED_EDGE('',*,*,#2538,.T.);
#3455=ORIENTED_EDGE('',*,*,#2535,.T.);
#3456=ORIENTED_EDGE('',*,*,#2525,.F.);
#3457=ORIENTED_EDGE('',*,*,#2485,.F.);
#3458=ORIENTED_EDGE('',*,*,#2526,.F.);
#3459=ORIENTED_EDGE('',*,*,#2550,.T.);
#3460=ORIENTED_EDGE('',*,*,#2549,.T.);
#3461=ORIENTED_EDGE('',*,*,#2550,.F.);
#3462=ORIENTED_EDGE('',*,*,#2499,.T.);
#3463=ORIENTED_EDGE('',*,*,#2522,.T.);
#3464=ORIENTED_EDGE('',*,*,#2551,.F.);
#3465=ORIENTED_EDGE('',*,*,#2530,.T.);
#3466=ORIENTED_EDGE('',*,*,#2552,.F.);
#3467=ORIENTED_EDGE('',*,*,#2553,.T.);
#3468=ORIENTED_EDGE('',*,*,#2519,.T.);
#3469=ORIENTED_EDGE('',*,*,#2551,.T.);
#3470=ORIENTED_EDGE('',*,*,#2520,.T.);
#3471=ORIENTED_EDGE('',*,*,#2553,.F.);
#3472=ORIENTED_EDGE('',*,*,#2552,.T.);
#4168=CONICAL_SURFACE('',#4837,0.9,0.785398163397448);
#4169=CONICAL_SURFACE('',#4840,0.875,0.896055384571344);
#4297=ADVANCED_FACE('',(#630),#456,.T.);
#4298=ADVANCED_FACE('',(#631),#457,.T.);
#4299=ADVANCED_FACE('',(#632),#458,.T.);
#4300=ADVANCED_FACE('',(#633),#459,.T.);
#4301=ADVANCED_FACE('',(#634),#460,.T.);
#4302=ADVANCED_FACE('',(#635),#461,.T.);
#4303=ADVANCED_FACE('',(#636),#462,.T.);
#4304=ADVANCED_FACE('',(#637),#463,.T.);
#4305=ADVANCED_FACE('',(#638),#464,.T.);
#4306=ADVANCED_FACE('',(#639),#465,.T.);
#4307=ADVANCED_FACE('',(#640),#466,.T.);
#4308=ADVANCED_FACE('',(#641),#369,.F.);
#4309=ADVANCED_FACE('',(#642),#80,.F.);
#4310=ADVANCED_FACE('',(#643),#370,.T.);
#4311=ADVANCED_FACE('',(#644),#467,.T.);
#4312=ADVANCED_FACE('',(#645),#81,.F.);
#4313=ADVANCED_FACE('',(#646),#371,.F.);
#4314=ADVANCED_FACE('',(#647),#372,.F.);
#4315=ADVANCED_FACE('',(#648),#373,.F.);
#4316=ADVANCED_FACE('',(#649),#374,.F.);
#4317=ADVANCED_FACE('',(#650),#375,.F.);
#4318=ADVANCED_FACE('',(#651),#376,.F.);
#4319=ADVANCED_FACE('',(#652),#377,.F.);
#4320=ADVANCED_FACE('',(#653,#306),#378,.T.);
#4321=ADVANCED_FACE('',(#654),#4168,.T.);
#4322=ADVANCED_FACE('',(#655),#468,.T.);
#4323=ADVANCED_FACE('',(#656),#4169,.T.);
#4324=ADVANCED_FACE('',(#657),#379,.T.);
#4466=CLOSED_SHELL('',(#4297,#4298,#4299,#4300,#4301,#4302,#4303,#4304,
#4305,#4306,#4307,#4308,#4309,#4310,#4311,#4312,#4313,#4314,#4315,#4316,
#4317,#4318,#4319,#4320,#4321,#4322,#4323,#4324));
#4806=AXIS2_PLACEMENT_3D('',#6924,#5584,#5585);
#4807=AXIS2_PLACEMENT_3D('',#6925,#5586,#5587);
#4808=AXIS2_PLACEMENT_3D('',#6941,#5589,#5590);
#4809=AXIS2_PLACEMENT_3D('',#6949,#5591,#5592);
#4810=AXIS2_PLACEMENT_3D('',#6997,#5594,#5595);
#4811=AXIS2_PLACEMENT_3D('',#7045,#5597,#5598);
#4812=AXIS2_PLACEMENT_3D('',#7093,#5600,#5601);
#4813=AXIS2_PLACEMENT_3D('',#7147,#5603,#5604);
#4814=AXIS2_PLACEMENT_3D('',#7195,#5606,#5607);
#4815=AXIS2_PLACEMENT_3D('',#7209,#5609,#5610);
#4816=AXIS2_PLACEMENT_3D('',#7217,#5611,#5612);
#4817=AXIS2_PLACEMENT_3D('',#7242,#5614,#5615);
#4818=AXIS2_PLACEMENT_3D('',#7267,#5617,#5618);
#4819=AXIS2_PLACEMENT_3D('',#7291,#5620,#5621);
#4820=AXIS2_PLACEMENT_3D('',#7315,#5623,#5624);
#4821=AXIS2_PLACEMENT_3D('',#7394,#5625,#5626);
#4822=AXIS2_PLACEMENT_3D('',#7396,#5627,#5628);
#4823=AXIS2_PLACEMENT_3D('',#7719,#5629,#5630);
#4824=AXIS2_PLACEMENT_3D('',#7721,#5631,#5632);
#4825=AXIS2_PLACEMENT_3D('',#7722,#5633,#5634);
#4826=AXIS2_PLACEMENT_3D('',#7797,#5635,#5636);
#4827=AXIS2_PLACEMENT_3D('',#7798,#5637,#5638);
#4828=AXIS2_PLACEMENT_3D('',#7967,#5639,#5640);
#4829=AXIS2_PLACEMENT_3D('',#7976,#5645,#5646);
#4830=AXIS2_PLACEMENT_3D('',#7982,#5650,#5651);
#4831=AXIS2_PLACEMENT_3D('',#7988,#5655,#5656);
#4832=AXIS2_PLACEMENT_3D('',#7994,#5660,#5661);
#4833=AXIS2_PLACEMENT_3D('',#8000,#5665,#5666);
#4834=AXIS2_PLACEMENT_3D('',#8003,#5669,#5670);
#4835=AXIS2_PLACEMENT_3D('',#8004,#5671,#5672);
#4836=AXIS2_PLACEMENT_3D('',#8006,#5673,#5674);
#4837=AXIS2_PLACEMENT_3D('',#8007,#5675,#5676);
#4838=AXIS2_PLACEMENT_3D('',#8009,#5678,#5679);
#4839=AXIS2_PLACEMENT_3D('',#8010,#5680,#5681);
#4840=AXIS2_PLACEMENT_3D('',#8011,#5682,#5683);
#4841=AXIS2_PLACEMENT_3D('',#8013,#5684,#5685);
#4842=AXIS2_PLACEMENT_3D('',#8015,#5687,#5688);
#5584=DIRECTION('axis',(0.,0.,1.));
#5585=DIRECTION('refdir',(1.,0.,0.));
#5586=DIRECTION('center_axis',(1.,0.,0.));
#5587=DIRECTION('ref_axis',(0.,1.,0.));
#5588=DIRECTION('',(-1.,0.,0.));
#5589=DIRECTION('center_axis',(1.,0.,0.));
#5590=DIRECTION('ref_axis',(0.,1.,0.));
#5591=DIRECTION('center_axis',(1.,0.,0.));
#5592=DIRECTION('ref_axis',(0.,1.,0.));
#5593=DIRECTION('',(-1.,0.,0.));
#5594=DIRECTION('center_axis',(1.,0.,0.));
#5595=DIRECTION('ref_axis',(0.,1.,0.));
#5596=DIRECTION('',(-1.,0.,0.));
#5597=DIRECTION('center_axis',(1.,0.,0.));
#5598=DIRECTION('ref_axis',(0.,1.,0.));
#5599=DIRECTION('',(-1.,0.,0.));
#5600=DIRECTION('center_axis',(1.,0.,0.));
#5601=DIRECTION('ref_axis',(0.,1.,0.));
#5602=DIRECTION('',(-1.,0.,0.));
#5603=DIRECTION('center_axis',(1.,0.,0.));
#5604=DIRECTION('ref_axis',(0.,1.,0.));
#5605=DIRECTION('',(-1.,0.,0.));
#5606=DIRECTION('center_axis',(1.,0.,0.));
#5607=DIRECTION('ref_axis',(9.38957226509774E-17,0.703402809462063,-0.710791451581177));
#5608=DIRECTION('',(1.,0.,0.));
#5609=DIRECTION('center_axis',(1.,0.,0.));
#5610=DIRECTION('ref_axis',(9.38957226509774E-17,1.,7.2918327227141E-15));
#5611=DIRECTION('center_axis',(1.,0.,0.));
#5612=DIRECTION('ref_axis',(9.38957226509774E-17,1.,7.2918327227141E-15));
#5613=DIRECTION('',(1.,0.,0.));
#5614=DIRECTION('center_axis',(1.,0.,0.));
#5615=DIRECTION('ref_axis',(9.38957226509774E-17,1.,7.2918327227141E-15));
#5616=DIRECTION('',(1.,0.,0.));
#5617=DIRECTION('center_axis',(1.,0.,0.));
#5618=DIRECTION('ref_axis',(9.38957226509774E-17,1.,7.2918327227141E-15));
#5619=DIRECTION('',(1.,0.,0.));
#5620=DIRECTION('center_axis',(1.,0.,0.));
#5621=DIRECTION('ref_axis',(9.38957226509774E-17,1.,7.2918327227141E-15));
#5622=DIRECTION('',(1.,0.,0.));
#5623=DIRECTION('center_axis',(1.,0.,0.));
#5624=DIRECTION('ref_axis',(0.,0.,-1.));
#5625=DIRECTION('center_axis',(-1.,0.,0.));
#5626=DIRECTION('ref_axis',(0.,1.,0.));
#5627=DIRECTION('center_axis',(-1.,0.,0.));
#5628=DIRECTION('ref_axis',(0.,1.,0.));
#5629=DIRECTION('center_axis',(1.,0.,0.));
#5630=DIRECTION('ref_axis',(0.,0.,-1.));
#5631=DIRECTION('center_axis',(1.,0.,0.));
#5632=DIRECTION('ref_axis',(0.,1.,0.));
#5633=DIRECTION('center_axis',(1.,0.,0.));
#5634=DIRECTION('ref_axis',(0.,1.,0.));
#5635=DIRECTION('center_axis',(-1.,0.,0.));
#5636=DIRECTION('ref_axis',(9.38957226509774E-17,1.,7.2918327227141E-15));
#5637=DIRECTION('center_axis',(1.,0.,0.));
#5638=DIRECTION('ref_axis',(9.38957226509774E-17,1.,7.2918327227141E-15));
#5639=DIRECTION('center_axis',(0.,0.5,-0.866025403784439));
#5640=DIRECTION('ref_axis',(0.,0.866025403784439,0.5));
#5641=DIRECTION('',(0.,0.866025403784439,0.5));
#5642=DIRECTION('',(1.,0.,0.));
#5643=DIRECTION('',(0.,0.866025403784439,0.5));
#5644=DIRECTION('',(1.,0.,0.));
#5645=DIRECTION('center_axis',(0.,-0.5,-0.866025403784439));
#5646=DIRECTION('ref_axis',(0.,0.866025403784439,-0.5));
#5647=DIRECTION('',(0.,0.866025403784439,-0.5));
#5648=DIRECTION('',(1.,0.,0.));
#5649=DIRECTION('',(0.,0.866025403784439,-0.5));
#5650=DIRECTION('center_axis',(0.,-1.,-1.33539075443303E-16));
#5651=DIRECTION('ref_axis',(0.,1.33539075443303E-16,-1.));
#5652=DIRECTION('',(0.,1.33539075443303E-16,-1.));
#5653=DIRECTION('',(1.,0.,0.));
#5654=DIRECTION('',(0.,1.33539075443303E-16,-1.));
#5655=DIRECTION('center_axis',(0.,-0.5,0.866025403784439));
#5656=DIRECTION('ref_axis',(0.,-0.866025403784439,-0.5));
#5657=DIRECTION('',(0.,-0.866025403784439,-0.5));
#5658=DIRECTION('',(1.,0.,0.));
#5659=DIRECTION('',(0.,-0.866025403784439,-0.5));
#5660=DIRECTION('center_axis',(0.,0.5,0.866025403784439));
#5661=DIRECTION('ref_axis',(0.,-0.866025403784439,0.5));
#5662=DIRECTION('',(0.,-0.866025403784439,0.5));
#5663=DIRECTION('',(1.,0.,0.));
#5664=DIRECTION('',(0.,-0.866025403784439,0.5));
#5665=DIRECTION('center_axis',(0.,1.,-2.67078150886606E-16));
#5666=DIRECTION('ref_axis',(0.,2.67078150886606E-16,1.));
#5667=DIRECTION('',(0.,2.67078150886606E-16,1.));
#5668=DIRECTION('',(0.,2.67078150886606E-16,1.));
#5669=DIRECTION('center_axis',(1.,0.,0.));
#5670=DIRECTION('ref_axis',(0.,0.,-1.));
#5671=DIRECTION('center_axis',(-1.,0.,0.));
#5672=DIRECTION('ref_axis',(0.,0.,1.));
#5673=DIRECTION('center_axis',(1.,0.,0.));
#5674=DIRECTION('ref_axis',(0.,0.,-1.));
#5675=DIRECTION('center_axis',(1.,0.,0.));
#5676=DIRECTION('ref_axis',(0.,1.,0.));
#5677=DIRECTION('',(-0.707106781186547,0.707106781186547,8.65956056235493E-17));
#5678=DIRECTION('center_axis',(1.,0.,0.));
#5679=DIRECTION('ref_axis',(0.,-0.766494216754321,-0.642251209171443));
#5680=DIRECTION('center_axis',(-1.,0.,0.));
#5681=DIRECTION('ref_axis',(0.,1.,0.));
#5682=DIRECTION('center_axis',(-1.,0.,0.));
#5683=DIRECTION('ref_axis',(0.,1.,0.));
#5684=DIRECTION('center_axis',(1.,0.,0.));
#5685=DIRECTION('ref_axis',(0.,0.,-1.));
#5686=DIRECTION('',(-0.624695047554424,-0.78086880944303,-9.56288488038411E-17));
#5687=DIRECTION('center_axis',(1.,0.,0.));
#5688=DIRECTION('ref_axis',(0.,0.,-1.));
#6924=CARTESIAN_POINT('',(0.,0.,0.));
#6925=CARTESIAN_POINT('Origin',(1.25,0.,0.));
#6926=CARTESIAN_POINT('',(0.295735916889676,-0.96799567585261,0.000586695936425057));
#6927=CARTESIAN_POINT('',(0.237764083110324,-0.96769285498825,0.00103535076607003));
#6928=CARTESIAN_POINT('',(1.25,-0.96675,-1.1839272930757E-16));
#6929=CARTESIAN_POINT('',(0.16675,0.425622873836743,0.868928367815379));
#6930=CARTESIAN_POINT('Ctrl Pts',(0.295735916889676,-0.96799567585261,0.000586695936425057));
#6931=CARTESIAN_POINT('Ctrl Pts',(0.29377460420558,-0.968188204818438,0.0302592824465942));
#6932=CARTESIAN_POINT('Ctrl Pts',(0.291813291521485,-0.966943036624424,
0.0599143163822494));
#6933=CARTESIAN_POINT('Ctrl Pts',(0.289851978837389,-0.964207634563732,
0.0894298058826106));
#6934=CARTESIAN_POINT('Ctrl Pts',(0.268635853616945,-0.934617945413966,
0.4087079741524));
#6935=CARTESIAN_POINT('Ctrl Pts',(0.247419728396501,-0.730649773407094,
0.711657465788388));
#6936=CARTESIAN_POINT('Ctrl Pts',(0.226203603176058,-0.445967050164715,
0.859445316294661));
#6937=CARTESIAN_POINT('Ctrl Pts',(0.206385735450705,-0.180046459373982,
0.997493147475694));
#6938=CARTESIAN_POINT('Ctrl Pts',(0.186567867725353,0.156300216529493,1.00015737338151));
#6939=CARTESIAN_POINT('Ctrl Pts',(0.16675,0.426126619158378,0.869594511950287));
#6940=CARTESIAN_POINT('',(0.16675,-0.425119128515107,0.868262223680471));
#6941=CARTESIAN_POINT('Origin',(0.16675,0.,0.));
#6942=CARTESIAN_POINT('Ctrl Pts',(0.16675,-0.425119128515108,0.868262223680471));
#6943=CARTESIAN_POINT('Ctrl Pts',(0.187966125220444,-0.714478034118649,
0.726586123507843));
#6944=CARTESIAN_POINT('Ctrl Pts',(0.209182250440888,-0.924905046764807,
0.430096049228702));
#6945=CARTESIAN_POINT('Ctrl Pts',(0.230398375661332,-0.961770620498793,
0.112067875014351));
#6946=CARTESIAN_POINT('Ctrl Pts',(0.232853611477663,-0.966036888541652,
0.0752640686727022));
#6947=CARTESIAN_POINT('Ctrl Pts',(0.235308847293994,-0.967978774477045,
0.0381718182248514));
#6948=CARTESIAN_POINT('Ctrl Pts',(0.237764083110324,-0.96769285498825,0.00103535076607003));
#6949=CARTESIAN_POINT('Origin',(1.25,0.,0.));
#6950=CARTESIAN_POINT('',(0.695735916889677,-0.965535960161722,0.000603907848525584));
#6951=CARTESIAN_POINT('',(0.637764083110324,-0.965403356746268,0.000512007511799884));
#6952=CARTESIAN_POINT('',(1.25,-0.96675,-1.1839272930757E-16));
#6953=CARTESIAN_POINT('Ctrl Pts',(0.695735916889677,-0.965535960161722,
0.000603907848525584));
#6954=CARTESIAN_POINT('Ctrl Pts',(0.687738022194911,-0.966226783953424,
0.12240713418347));
#6955=CARTESIAN_POINT('Ctrl Pts',(0.679740127500145,-0.944877535015784,
0.243976853099216));
#6956=CARTESIAN_POINT('Ctrl Pts',(0.671742232805379,-0.900384620032069,
0.356385477320749));
#6957=CARTESIAN_POINT('Ctrl Pts',(0.650526107584935,-0.782357652718426,
0.654573380307598));
#6958=CARTESIAN_POINT('Ctrl Pts',(0.629309982364491,-0.501471247814132,
0.888295665503207));
#6959=CARTESIAN_POINT('Ctrl Pts',(0.608093857144047,-0.186796400447701,
0.950160710409515));
#6960=CARTESIAN_POINT('Ctrl Pts',(0.586877731923603,0.127878446918726,1.01202575531582));
#6961=CARTESIAN_POINT('Ctrl Pts',(0.565661606703159,0.47634173674729,0.902033559932829));
#6962=CARTESIAN_POINT('Ctrl Pts',(0.544445481482716,0.698465791461622,0.670712394137428));
#6963=CARTESIAN_POINT('Ctrl Pts',(0.523229356262272,0.920589846175955,0.439391228342025));
#6964=CARTESIAN_POINT('Ctrl Pts',(0.502013231041828,1.01637466577606,0.0867410921342136));
#6965=CARTESIAN_POINT('Ctrl Pts',(0.480797105821384,0.941810253427243,-0.225160240747506));
#6966=CARTESIAN_POINT('Ctrl Pts',(0.45958098060094,0.867245841078429,-0.537061573629225));
#6967=CARTESIAN_POINT('Ctrl Pts',(0.438364855380496,0.622332196780702,-0.808214103184852));
#6968=CARTESIAN_POINT('Ctrl Pts',(0.417148730160052,0.319602326501539,-0.914072937871646));
#6969=CARTESIAN_POINT('Ctrl Pts',(0.395932604939608,0.0168724562223755,
-1.01993177255844));
#6970=CARTESIAN_POINT('Ctrl Pts',(0.374716479719165,-0.343673640038224,
-0.960496912376401));
#6971=CARTESIAN_POINT('Ctrl Pts',(0.353500354498721,-0.596341085022193,
-0.762976059833586));
#6972=CARTESIAN_POINT('Ctrl Pts',(0.334245541962373,-0.825650831107044,
-0.583714910673945));
#6973=CARTESIAN_POINT('Ctrl Pts',(0.314990729426024,-0.966105559516294,
-0.290718252710928));
#6974=CARTESIAN_POINT('Ctrl Pts',(0.295735916889676,-0.96799567585261,0.000586695936425057));
#6975=CARTESIAN_POINT('Ctrl Pts',(0.237764083110324,-0.96769285498825,0.00103535076607003));
#6976=CARTESIAN_POINT('Ctrl Pts',(0.256524972514437,-0.965508093804783,
-0.282730939306557));
#6977=CARTESIAN_POINT('Ctrl Pts',(0.275285861918551,-0.833247180307396,
-0.569078953342249));
#6978=CARTESIAN_POINT('Ctrl Pts',(0.294046751322664,-0.613997775944128,
-0.74904683801851));
#6979=CARTESIAN_POINT('Ctrl Pts',(0.315262876543107,-0.366055222833664,
-0.952567102687459));
#6980=CARTESIAN_POINT('Ctrl Pts',(0.336479001763551,-0.00686598179092317,
-1.02004135787579));
#6981=CARTESIAN_POINT('Ctrl Pts',(0.357695126983995,0.298275211789835,-0.921175933203103));
#6982=CARTESIAN_POINT('Ctrl Pts',(0.378911252204439,0.603416405370592,-0.822310508530412));
#6983=CARTESIAN_POINT('Ctrl Pts',(0.400127377424883,0.854509551489366,-0.557105403996695));
#6984=CARTESIAN_POINT('Ctrl Pts',(0.421343502645326,0.936297417272776,-0.247065280132184));
#6985=CARTESIAN_POINT('Ctrl Pts',(0.44255962786577,1.01808528305619,0.0629748437323275));
#6986=CARTESIAN_POINT('Ctrl Pts',(0.463775753086214,0.93056786850423,0.417849986927633));
#6987=CARTESIAN_POINT('Ctrl Pts',(0.484991878306658,0.713895687898178,0.654299743496954));
#6988=CARTESIAN_POINT('Ctrl Pts',(0.506208003527102,0.497223507292127,0.890749500066273));
#6989=CARTESIAN_POINT('Ctrl Pts',(0.527424128747546,0.151396560631982,1.00877387000961));
#6990=CARTESIAN_POINT('Ctrl Pts',(0.54864025396799,-0.16463713113037,0.954237787400182));
#6991=CARTESIAN_POINT('Ctrl Pts',(0.569856379188434,-0.480670822892721,
0.899701704790755));
#6992=CARTESIAN_POINT('Ctrl Pts',(0.591072504408878,-0.766911259757278,
0.672605169628564));
#6993=CARTESIAN_POINT('Ctrl Pts',(0.612288629629321,-0.891843900121912,
0.377250898045158));
#6994=CARTESIAN_POINT('Ctrl Pts',(0.620780447456322,-0.941848564574043,
0.259034463957746));
#6995=CARTESIAN_POINT('Ctrl Pts',(0.629272265283323,-0.966011322203064,
0.129882972155661));
#6996=CARTESIAN_POINT('Ctrl Pts',(0.637764083110324,-0.965403356746268,
0.000512007511799884));
#6997=CARTESIAN_POINT('Origin',(1.25,0.,0.));
#6998=CARTESIAN_POINT('',(1.09573591688968,-0.965800633193088,-0.00073910647511409));
#6999=CARTESIAN_POINT('',(1.03776408311032,-0.965986601461759,-0.000802905574952835));
#7000=CARTESIAN_POINT('',(1.25,-0.96675,-1.1839272930757E-16));
#7001=CARTESIAN_POINT('Ctrl Pts',(1.09573591688968,-0.965800633193088,-0.00073910647511409));
#7002=CARTESIAN_POINT('Ctrl Pts',(1.08170144018424,-0.964287961650603,0.212850295800185));
#7003=CARTESIAN_POINT('Ctrl Pts',(1.0676669634788,-0.894477007693264,0.427337796170151));
#7004=CARTESIAN_POINT('Ctrl Pts',(1.05363248677337,-0.764181677306994,0.594751173789774));
#7005=CARTESIAN_POINT('Ctrl Pts',(1.03241636155292,-0.567212306582722,0.847832443416278));
#7006=CARTESIAN_POINT('Ctrl Pts',(1.01120023633248,-0.232019113166176,0.993336094150022));
#7007=CARTESIAN_POINT('Ctrl Pts',(0.989984111112037,0.0873706532867941,
0.964400766431873));
#7008=CARTESIAN_POINT('Ctrl Pts',(0.968767985891593,0.406760419739764,0.935465438713724));
#7009=CARTESIAN_POINT('Ctrl Pts',(0.947551860671148,0.71034675922916,0.732091132543686));
#7010=CARTESIAN_POINT('Ctrl Pts',(0.926335735450704,0.858626252065649,0.447731661748216));
#7011=CARTESIAN_POINT('Ctrl Pts',(0.90511961023026,1.00690574490214,0.163372190952747));
#7012=CARTESIAN_POINT('Ctrl Pts',(0.883903485009817,0.999878391085719,-0.201972444468155));
#7013=CARTESIAN_POINT('Ctrl Pts',(0.862687359789374,0.840773489282268,-0.480419223503817));
#7014=CARTESIAN_POINT('Ctrl Pts',(0.84147123456893,0.681668587478818,-0.758866002539479));
#7015=CARTESIAN_POINT('Ctrl Pts',(0.820255109348486,0.370486137688336,-0.950414925189903));
#7016=CARTESIAN_POINT('Ctrl Pts',(0.799038984128042,0.0502198570115047,
-0.967046989745439));
#7017=CARTESIAN_POINT('Ctrl Pts',(0.777822858907598,-0.270046423665327,
-0.983679054300974));
#7018=CARTESIAN_POINT('Ctrl Pts',(0.756606733687153,-0.599396535228511,
-0.82539426076162));
#7019=CARTESIAN_POINT('Ctrl Pts',(0.73539060846671,-0.786487826148606,-0.564925103602899));
#7020=CARTESIAN_POINT('Ctrl Pts',(0.722172377941032,-0.903050854837064,
-0.402645642656119));
#7021=CARTESIAN_POINT('Ctrl Pts',(0.708954147415354,-0.96439422618299,-0.200701958996695));
#7022=CARTESIAN_POINT('Ctrl Pts',(0.695735916889677,-0.965535960161722,
0.000603907848525584));
#7023=CARTESIAN_POINT('Ctrl Pts',(0.637764083110324,-0.965403356746268,
0.000512007511799884));
#7024=CARTESIAN_POINT('Ctrl Pts',(0.650488390503767,-0.964492369309365,
-0.193339998672378));
#7025=CARTESIAN_POINT('Ctrl Pts',(0.66321269789721,-0.907964626205851,-0.387684778820973));
#7026=CARTESIAN_POINT('Ctrl Pts',(0.675937005290653,-0.79942395847086,-0.546471414702047));
#7027=CARTESIAN_POINT('Ctrl Pts',(0.697153130511097,-0.618446532590466,
-0.811227447861222));
#7028=CARTESIAN_POINT('Ctrl Pts',(0.71836925573154,-0.292866836964969,-0.977127506174948));
#7029=CARTESIAN_POINT('Ctrl Pts',(0.739585380951984,0.0277004179809616,
-0.967951999615512));
#7030=CARTESIAN_POINT('Ctrl Pts',(0.760801506172428,0.348267672926892,-0.958776493056076));
#7031=CARTESIAN_POINT('Ctrl Pts',(0.782017631392872,0.663822487193254,-0.774525421623477));
#7032=CARTESIAN_POINT('Ctrl Pts',(0.803233756613316,0.829364401714287,-0.49985784471143));
#7033=CARTESIAN_POINT('Ctrl Pts',(0.82444988183376,0.99490631623532,-0.225190267799384));
#7034=CARTESIAN_POINT('Ctrl Pts',(0.845666007054203,1.01043533101103,0.13989381459211));
#7035=CARTESIAN_POINT('Ctrl Pts',(0.866882132274647,0.868814199090254,0.427627717529623));
#7036=CARTESIAN_POINT('Ctrl Pts',(0.888098257495091,0.727193067169481,0.715361620467137));
#7037=CARTESIAN_POINT('Ctrl Pts',(0.909314382715535,0.428421788552229,0.925745343950671));
#7038=CARTESIAN_POINT('Ctrl Pts',(0.930530507935979,0.109791850608296,0.962105904569766));
#7039=CARTESIAN_POINT('Ctrl Pts',(0.951746633156423,-0.208838087335635,
0.99846646518886));
#7040=CARTESIAN_POINT('Ctrl Pts',(0.972962758376867,-0.547326684606245,
0.86080386294352));
#7041=CARTESIAN_POINT('Ctrl Pts',(0.99417888359731,-0.750132748216865,0.612375420712454));
#7042=CARTESIAN_POINT('Ctrl Pts',(1.00870728343498,-0.889010491019784,0.442256339010159));
#7043=CARTESIAN_POINT('Ctrl Pts',(1.02323568327265,-0.964263295846235,0.220196380992393));
#7044=CARTESIAN_POINT('Ctrl Pts',(1.03776408311032,-0.965986601461759,-0.000802905574952835));
#7045=CARTESIAN_POINT('Origin',(1.25,0.,0.));
#7046=CARTESIAN_POINT('',(1.49573591688968,-0.968224609176391,-0.00031821983524985));
#7047=CARTESIAN_POINT('',(1.43776408311032,-0.96830804582958,-0.000184094457921295));
#7048=CARTESIAN_POINT('',(1.25,-0.96675,-1.1839272930757E-16));
#7049=CARTESIAN_POINT('Ctrl Pts',(1.49573591688968,-0.968224609176391,-0.00031821983524985));
#7050=CARTESIAN_POINT('Ctrl Pts',(1.47566485817357,-0.966926994481933,0.3031765508298));
#7051=CARTESIAN_POINT('Ctrl Pts',(1.45559379945746,-0.812598430180798,0.607808692581674));
#7052=CARTESIAN_POINT('Ctrl Pts',(1.43552274074136,-0.566555587107941,0.785313598752052));
#7053=CARTESIAN_POINT('Ctrl Pts',(1.41430661552091,-0.306475845323378,0.972945271292166));
#7054=CARTESIAN_POINT('Ctrl Pts',(1.39309049030047,0.0560813988977043,1.01853056055889));
#7055=CARTESIAN_POINT('Ctrl Pts',(1.37187436508003,0.354514689861907,0.901122524422879));
#7056=CARTESIAN_POINT('Ctrl Pts',(1.35065823985958,0.65294798082611,0.783714488286868));
#7057=CARTESIAN_POINT('Ctrl Pts',(1.32944211463914,0.887257318533434,0.503313126748121));
#7058=CARTESIAN_POINT('Ctrl Pts',(1.30822598941869,0.949773311073654,0.188767720302581));
#7059=CARTESIAN_POINT('Ctrl Pts',(1.28700986419825,1.01228930361387,-0.125777686142959));
#7060=CARTESIAN_POINT('Ctrl Pts',(1.26579373897781,0.903011950986991,-0.474467137495291));
#7061=CARTESIAN_POINT('Ctrl Pts',(1.24457761375736,0.672156184097886,-0.697071481701902));
#7062=CARTESIAN_POINT('Ctrl Pts',(1.22336148853692,0.441300417208782,-0.919675825908513));
#7063=CARTESIAN_POINT('Ctrl Pts',(1.20214536331647,0.088866236057456,-1.0161950629694));
#7064=CARTESIAN_POINT('Ctrl Pts',(1.18092923809603,-0.223196554351772,-0.942276943640678));
#7065=CARTESIAN_POINT('Ctrl Pts',(1.15971311287559,-0.535259344761003,-0.868358824311952));
#7066=CARTESIAN_POINT('Ctrl Pts',(1.13849698765514,-0.806950744428136,-0.624003348593605));
#7067=CARTESIAN_POINT('Ctrl Pts',(1.1172808624347,-0.913423670245701,-0.321496166474798));
#7068=CARTESIAN_POINT('Ctrl Pts',(1.11009921391969,-0.949464706091843,-0.219097626087732));
#7069=CARTESIAN_POINT('Ctrl Pts',(1.10291756540468,-0.966574689509172,-0.110035950658669));
#7070=CARTESIAN_POINT('Ctrl Pts',(1.09573591688968,-0.965800633193088,-0.00073910647511409));
#7071=CARTESIAN_POINT('Ctrl Pts',(1.03776408311032,-0.965986601461759,-0.000802905574952835));
#7072=CARTESIAN_POINT('Ctrl Pts',(1.0444518084931,-0.966779874969921,-0.10253348532667));
#7073=CARTESIAN_POINT('Ctrl Pts',(1.05113953387587,-0.951992594196094,-0.204039313797799));
#7074=CARTESIAN_POINT('Ctrl Pts',(1.05782725925864,-0.92065867003448,-0.300150629635464));
#7075=CARTESIAN_POINT('Ctrl Pts',(1.07904338447909,-0.821254998290845,-0.605053955535511));
#7076=CARTESIAN_POINT('Ctrl Pts',(1.10025950969953,-0.55532412485295,-0.855666325118811));
#7077=CARTESIAN_POINT('Ctrl Pts',(1.12147563491997,-0.245066160482458,-0.936827173206812));
#7078=CARTESIAN_POINT('Ctrl Pts',(1.14269176014042,0.0651918038880355,-1.01798802129481));
#7079=CARTESIAN_POINT('Ctrl Pts',(1.16390788536086,0.419776859191126,-0.929697347887511));
#7080=CARTESIAN_POINT('Ctrl Pts',(1.1851240105813,0.655750876121149,-0.712526132007322));
#7081=CARTESIAN_POINT('Ctrl Pts',(1.20634013580175,0.891724893051173,-0.495354916127132));
#7082=CARTESIAN_POINT('Ctrl Pts',(1.22755626102219,1.00908787160813,-0.149303157774051));
#7083=CARTESIAN_POINT('Ctrl Pts',(1.24877238624264,0.953909384255206,0.166612060731162));
#7084=CARTESIAN_POINT('Ctrl Pts',(1.26998851146308,0.898730896902285,0.482527279236372));
#7085=CARTESIAN_POINT('Ctrl Pts',(1.29120463668352,0.671010943639489,0.768305957893716));
#7086=CARTESIAN_POINT('Ctrl Pts',(1.31242076190397,0.37539095120197,0.892627738781783));
#7087=CARTESIAN_POINT('Ctrl Pts',(1.33363688712441,0.079770958764452,1.01694951966985));
#7088=CARTESIAN_POINT('Ctrl Pts',(1.35485301234486,-0.283749072847788,0.979814402788641));
#7089=CARTESIAN_POINT('Ctrl Pts',(1.3760691375653,-0.548125202840523,0.798286573958416));
#7090=CARTESIAN_POINT('Ctrl Pts',(1.39663411941364,-0.804387374087343,0.622330009502189));
#7091=CARTESIAN_POINT('Ctrl Pts',(1.41719910126198,-0.967497900740498,0.310707828041999));
#7092=CARTESIAN_POINT('Ctrl Pts',(1.43776408311032,-0.96830804582958,-0.000184094457921295));
#7093=CARTESIAN_POINT('Origin',(1.25,0.,0.));
#7094=CARTESIAN_POINT('',(1.89573591688968,-0.966772019097869,0.00089209288056849));
#7095=CARTESIAN_POINT('',(1.83776408311032,-0.966544636178151,0.000891803094726289));
#7096=CARTESIAN_POINT('',(1.25,-0.96675,-1.1839272930757E-16));
#7097=CARTESIAN_POINT('Ctrl Pts',(1.89573591688968,-0.966772019097869,0.00089209288056849));
#7098=CARTESIAN_POINT('Ctrl Pts',(1.89084440138334,-0.967460921137827,0.0751428608741927));
#7099=CARTESIAN_POINT('Ctrl Pts',(1.88595288587701,-0.9596331226977,0.14925049718403));
#7100=CARTESIAN_POINT('Ctrl Pts',(1.88106137037068,-0.94274069279519,0.221232171309253));
#7101=CARTESIAN_POINT('Ctrl Pts',(1.85984524515023,-0.869472621248606,0.533440567631582));
#7102=CARTESIAN_POINT('Ctrl Pts',(1.83862911992979,-0.625676658048714,0.80565441474566));
#7103=CARTESIAN_POINT('Ctrl Pts',(1.81741299470935,-0.323389969041022,0.9127587334095));
#7104=CARTESIAN_POINT('Ctrl Pts',(1.7961968694889,-0.0211032800333296,1.01986305207334));
#7105=CARTESIAN_POINT('Ctrl Pts',(1.77498074426846,0.339674134782163,0.961857842286945));
#7106=CARTESIAN_POINT('Ctrl Pts',(1.75376461904802,0.59316308795535,0.765412190857585));
#7107=CARTESIAN_POINT('Ctrl Pts',(1.73254849382757,0.84665204112854,0.568966539428222));
#7108=CARTESIAN_POINT('Ctrl Pts',(1.71133236860713,0.992852532659421,0.234080446355895));
#7109=CARTESIAN_POINT('Ctrl Pts',(1.69011624338668,0.964580446894972,-0.0853676396729285));
#7110=CARTESIAN_POINT('Ctrl Pts',(1.66890011816624,0.936308361130523,-0.404815725701751));
#7111=CARTESIAN_POINT('Ctrl Pts',(1.6476839929458,0.733563698070743,-0.708825804687068));
#7112=CARTESIAN_POINT('Ctrl Pts',(1.62646786772535,0.449512511554961,-0.857695735862234));
#7113=CARTESIAN_POINT('Ctrl Pts',(1.60525174250491,0.16546132503918,-1.0065656670374));
#7114=CARTESIAN_POINT('Ctrl Pts',(1.58403561728446,-0.199896384932602,-1.00029545040241));
#7115=CARTESIAN_POINT('Ctrl Pts',(1.56281949206402,-0.478672858699194,-0.841768500692864));
#7116=CARTESIAN_POINT('Ctrl Pts',(1.54160336684358,-0.757449332465786,-0.683241550983313));
#7117=CARTESIAN_POINT('Ctrl Pts',(1.52038724162313,-0.949644570027188,-0.372457868199196));
#7118=CARTESIAN_POINT('Ctrl Pts',(1.49917111640269,-0.966941069133869,-0.0522269989003843));
#7119=CARTESIAN_POINT('Ctrl Pts',(1.49802604989835,-0.967874587463138,-0.0349436524703006));
#7120=CARTESIAN_POINT('Ctrl Pts',(1.49688098339401,-0.968298638909609,-0.0176327870957842));
#7121=CARTESIAN_POINT('Ctrl Pts',(1.49573591688968,-0.968224609176391,-0.00031821983524985));
#7122=CARTESIAN_POINT('Ctrl Pts',(1.43776408311032,-0.96830804582958,-0.000184094457921295));
#7123=CARTESIAN_POINT('Ctrl Pts',(1.43841522648243,-0.968333697231029,-0.0100277800137327));
#7124=CARTESIAN_POINT('Ctrl Pts',(1.43906636985453,-0.968196637926884,-0.0198707334643601));
#7125=CARTESIAN_POINT('Ctrl Pts',(1.43971751322663,-0.967894672944393,-0.0297086252262958));
#7126=CARTESIAN_POINT('Ctrl Pts',(1.46093363844708,-0.958055784682296,-0.350255454801532));
#7127=CARTESIAN_POINT('Ctrl Pts',(1.48214976366752,-0.773145779784875,-0.665428573172762));
#7128=CARTESIAN_POINT('Ctrl Pts',(1.50336588888796,-0.49813419844903,-0.83040044304409));
#7129=CARTESIAN_POINT('Ctrl Pts',(1.52458201410841,-0.223122617113181,-0.99537231291542));
#7130=CARTESIAN_POINT('Ctrl Pts',(1.54579813932885,0.141990540661093,-1.01014293428684));
#7131=CARTESIAN_POINT('Ctrl Pts',(1.56701426454929,0.429429381136857,-0.867924647533782));
#7132=CARTESIAN_POINT('Ctrl Pts',(1.58823038976974,0.716868221612619,-0.72570636078072));
#7133=CARTESIAN_POINT('Ctrl Pts',(1.60944651499018,0.926632744789872,-0.426499165903169));
#7134=CARTESIAN_POINT('Ctrl Pts',(1.63066264021063,0.962332115966355,-0.10779468641756));
#7135=CARTESIAN_POINT('Ctrl Pts',(1.65187876543107,0.998031487142837,0.210909793068051));
#7136=CARTESIAN_POINT('Ctrl Pts',(1.67309489065152,0.859665706318551,0.549111557161723));
#7137=CARTESIAN_POINT('Ctrl Pts',(1.69431101587196,0.610816854431274,0.751401884753216));
#7138=CARTESIAN_POINT('Ctrl Pts',(1.7155271410924,0.361968002543998,0.953692212344708));
#7139=CARTESIAN_POINT('Ctrl Pts',(1.73674326631284,0.00263607959373437,
1.02007110343402));
#7140=CARTESIAN_POINT('Ctrl Pts',(1.75795939153329,-0.302060451690969,0.920034271570729));
#7141=CARTESIAN_POINT('Ctrl Pts',(1.77917551675373,-0.606756982975677,0.819997439707436));
#7142=CARTESIAN_POINT('Ctrl Pts',(1.80039164197418,-0.856818122594822,0.553544884891533));
#7143=CARTESIAN_POINT('Ctrl Pts',(1.82160776719462,-0.937334401881812,0.243120124217056));
#7144=CARTESIAN_POINT('Ctrl Pts',(1.82699320583319,-0.95777241669368,0.164322818717865));
#7145=CARTESIAN_POINT('Ctrl Pts',(1.83237864447176,-0.967286105479931,0.0826922411753721));
#7146=CARTESIAN_POINT('Ctrl Pts',(1.83776408311032,-0.966544636178151,0.000891803094726289));
#7147=CARTESIAN_POINT('Origin',(1.25,0.,0.));
#7148=CARTESIAN_POINT('',(2.29573591688968,-0.964716333291436,0.000839189083712686));
#7149=CARTESIAN_POINT('',(2.23776408311032,-0.965144827742031,-0.000120440973035392));
#7150=CARTESIAN_POINT('',(1.25,-0.96675,-1.1839272930757E-16));
#7151=CARTESIAN_POINT('Ctrl Pts',(2.29573591688968,-0.964651808581398,0.000865815094782327));
#7152=CARTESIAN_POINT('Ctrl Pts',(2.28480781937267,-0.964804709789736,0.167104793299758));
#7153=CARTESIAN_POINT('Ctrl Pts',(2.27387972185567,-0.924102274326781,0.333140176983196));
#7154=CARTESIAN_POINT('Ctrl Pts',(2.26295162433867,-0.842840346924172,0.476636691321465));
#7155=CARTESIAN_POINT('Ctrl Pts',(2.24173549911822,-0.685076086059376,0.755224982848065));
#7156=CARTESIAN_POINT('Ctrl Pts',(2.22051937389778,-0.374437158674562,0.948860974182947));
#7157=CARTESIAN_POINT('Ctrl Pts',(2.19930324867734,-0.0541774433576252,
0.967020857490355));
#7158=CARTESIAN_POINT('Ctrl Pts',(2.17808712345689,0.266082271959314,0.985180740797765));
#7159=CARTESIAN_POINT('Ctrl Pts',(2.15687099823645,0.595962775208374,0.827864516077699));
#7160=CARTESIAN_POINT('Ctrl Pts',(2.135654873016,0.784103890128058,0.568079176717024));
#7161=CARTESIAN_POINT('Ctrl Pts',(2.11443874779556,0.97224500504774,0.308293837356353));
#7162=CARTESIAN_POINT('Ctrl Pts',(2.09322262257512,1.01864673163805,-0.0539606166449227));
#7163=CARTESIAN_POINT('Ctrl Pts',(2.07200649735467,0.901873588961803,-0.352587694431253));
#7164=CARTESIAN_POINT('Ctrl Pts',(2.05079037213423,0.785100446285557,-0.651214772217586));
#7165=CARTESIAN_POINT('Ctrl Pts',(2.02957424691379,0.505152434342748,-0.886214473788973));
#7166=CARTESIAN_POINT('Ctrl Pts',(2.00835812169334,0.190729503949967,-0.949408981360314));
#7167=CARTESIAN_POINT('Ctrl Pts',(1.9871419964729,-0.123693426442815,-1.01260348893165));
#7168=CARTESIAN_POINT('Ctrl Pts',(1.96592587125245,-0.472591275285571,-0.90399280250295));
#7169=CARTESIAN_POINT('Ctrl Pts',(1.94470974603201,-0.695670109760311,-0.673585986523306));
#7170=CARTESIAN_POINT('Ctrl Pts',(1.9283851363179,-0.867316669650043,-0.496300958873));
#7171=CARTESIAN_POINT('Ctrl Pts',(1.91206052660379,-0.964472924488232,-0.246907348192393));
#7172=CARTESIAN_POINT('Ctrl Pts',(1.89573591688968,-0.966772019097869,0.00089209288056849));
#7173=CARTESIAN_POINT('Ctrl Pts',(1.83776408311032,-0.966544636178151,0.000891803094726289));
#7174=CARTESIAN_POINT('Ctrl Pts',(1.8535947696922,-0.964365061047076,-0.239563466090049));
#7175=CARTESIAN_POINT('Ctrl Pts',(1.86942545627408,-0.873572025317322,-0.481486477651458));
#7176=CARTESIAN_POINT('Ctrl Pts',(1.88525614285595,-0.711162484222502,-0.657226222658887));
#7177=CARTESIAN_POINT('Ctrl Pts',(1.9064722680764,-0.493502868321361,-0.892750842327313));
#7178=CARTESIAN_POINT('Ctrl Pts',(1.92768839329684,-0.147212217564238,-1.00940311513113));
#7179=CARTESIAN_POINT('Ctrl Pts',(1.94890451851728,0.168589541409646,-0.953565539955677));
#7180=CARTESIAN_POINT('Ctrl Pts',(1.97012064373773,0.484391300383536,-0.897727964780228));
#7181=CARTESIAN_POINT('Ctrl Pts',(1.99133676895817,0.769704167574187,-0.669400541625513));
#7182=CARTESIAN_POINT('Ctrl Pts',(2.01255289417862,0.893408780830026,-0.373529828255184));
#7183=CARTESIAN_POINT('Ctrl Pts',(2.03376901939906,1.01711339408586,-0.0776591148848542));
#7184=CARTESIAN_POINT('Ctrl Pts',(2.0549851446195,0.979209753406891,0.285754888701089));
#7185=CARTESIAN_POINT('Ctrl Pts',(2.07620126983995,0.797139938097043,0.549766367596159));
#7186=CARTESIAN_POINT('Ctrl Pts',(2.09741739506039,0.615070122787196,0.813777846491227));
#7187=CARTESIAN_POINT('Ctrl Pts',(2.11863352028083,0.288834132846476,0.978386800695422));
#7188=CARTESIAN_POINT('Ctrl Pts',(2.13984964550128,-0.0317036593373814,
0.967858504908859));
#7189=CARTESIAN_POINT('Ctrl Pts',(2.16106577072172,-0.352241451521237,0.957330209122296));
#7190=CARTESIAN_POINT('Ctrl Pts',(2.18228189594217,-0.667081045948231,0.771664663344978));
#7191=CARTESIAN_POINT('Ctrl Pts',(2.20349802116261,-0.831458666207518,0.496357323535052));
#7192=CARTESIAN_POINT('Ctrl Pts',(2.21492004181185,-0.919953834546034,0.348141469437165));
#7193=CARTESIAN_POINT('Ctrl Pts',(2.22634206246109,-0.964839564100767,0.173944111700515));
#7194=CARTESIAN_POINT('Ctrl Pts',(2.23776408311032,-0.965144827742031,-0.000120440973035392));
#7195=CARTESIAN_POINT('Origin',(-0.572772559302386,0.,0.));
#7196=CARTESIAN_POINT('',(2.02722744069761,-0.739016831769666,0.000681930839134881));
#7197=CARTESIAN_POINT('',(2.10627255930239,-0.737772979261817,-9.20671105089643E-5));
#7198=CARTESIAN_POINT('',(-0.572772559302386,-0.739,-5.47916578054271E-15));
#7199=CARTESIAN_POINT('',(2.3266,0.00705397816592627,0.740208249496393));
#7200=CARTESIAN_POINT('Ctrl Pts',(2.02722744069761,-0.739016831769666,0.000681930839134901));
#7201=CARTESIAN_POINT('Ctrl Pts',(2.04355205041173,-0.737259365085908,-0.188740139968123));
#7202=CARTESIAN_POINT('Ctrl Pts',(2.08109278534628,-0.566469936104065,-0.627145185848076));
#7203=CARTESIAN_POINT('Ctrl Pts',(2.13984964550128,0.172150057567682,-0.857075020006521));
#7204=CARTESIAN_POINT('Ctrl Pts',(2.20349802116261,0.814140998842262,-0.318161817644216));
#7205=CARTESIAN_POINT('Ctrl Pts',(2.26574813932885,0.710067894618011,0.494328326954158));
#7206=CARTESIAN_POINT('Ctrl Pts',(2.30678213227465,0.23616540058745,0.736897610753465));
#7207=CARTESIAN_POINT('Ctrl Pts',(2.3266,0.00705185163866651,0.740219785066309));
#7208=CARTESIAN_POINT('',(2.3266,0.701646902936369,0.231975480600434));
#7209=CARTESIAN_POINT('Origin',(2.3266,0.,0.));
#7210=CARTESIAN_POINT('Ctrl Pts',(2.10627255930239,-0.737772979261817,-9.2067110508921E-5));
#7211=CARTESIAN_POINT('Ctrl Pts',(2.11606666387359,-0.737973070067811,-0.114185958198688));
#7212=CARTESIAN_POINT('Ctrl Pts',(2.14707689366524,-0.65927271946186,-0.475195283900803));
#7213=CARTESIAN_POINT('Ctrl Pts',(2.19930324867733,-0.0957849414937873,
-0.86944400077431));
#7214=CARTESIAN_POINT('Ctrl Pts',(2.26295162433867,0.68001209321599,-0.548823559975255));
#7215=CARTESIAN_POINT('Ctrl Pts',(2.30538387477956,0.778955542380413,-0.00185685071207135));
#7216=CARTESIAN_POINT('Ctrl Pts',(2.3266,0.701646902936369,0.231975480600434));
#7217=CARTESIAN_POINT('Origin',(-0.572772559302386,0.,0.));
#7218=CARTESIAN_POINT('',(1.62722744069761,-0.740127216117252,-0.000243252607449027));
#7219=CARTESIAN_POINT('',(1.70627255930239,-0.738843016432018,0.000681709321951329));
#7220=CARTESIAN_POINT('',(-0.572772559302386,-0.739,-5.47916578054271E-15));
#7221=CARTESIAN_POINT('Ctrl Pts',(1.62722744069761,-0.740127216117252,-0.000243252607449037));
#7222=CARTESIAN_POINT('Ctrl Pts',(1.62837250720195,-0.740183805693511,-0.013478799755662));
#7223=CARTESIAN_POINT('Ctrl Pts',(1.65073369892673,-0.73385366968859,-0.271891153010392));
#7224=CARTESIAN_POINT('Ctrl Pts',(1.69431101587196,-0.432089760676844,-0.759849648569051));
#7225=CARTESIAN_POINT('Ctrl Pts',(1.75795939153329,0.405767020298013,-0.774228826515532));
#7226=CARTESIAN_POINT('Ctrl Pts',(1.82160776719462,0.870711336826102,-0.0770575359952864));
#7227=CARTESIAN_POINT('Ctrl Pts',(1.88525614285595,0.535436974556678,0.690920191795093));
#7228=CARTESIAN_POINT('Ctrl Pts',(1.94890451851728,-0.291916041885991,0.823940672887867));
#7229=CARTESIAN_POINT('Ctrl Pts',(1.9962282844645,-0.707606442547758,0.359795648961634));
#7230=CARTESIAN_POINT('Ctrl Pts',(2.02233592519128,-0.739543440104323,0.0574404698071101));
#7231=CARTESIAN_POINT('Ctrl Pts',(2.02722744069761,-0.739016831769666,0.000681930839134901));
#7232=CARTESIAN_POINT('Ctrl Pts',(1.70627255930239,-0.738843016432019,0.000681709321951364));
#7233=CARTESIAN_POINT('Ctrl Pts',(1.72210324588426,-0.737176912452845,-0.18312635266672));
#7234=CARTESIAN_POINT('Ctrl Pts',(1.75915005768658,-0.574759015302088,-0.615897726532182));
#7235=CARTESIAN_POINT('Ctrl Pts',(1.81741299470935,0.152178910917555,-0.860775724524354));
#7236=CARTESIAN_POINT('Ctrl Pts',(1.88106137037068,0.806472809610774,-0.33716372852332));
#7237=CARTESIAN_POINT('Ctrl Pts',(1.94470974603201,0.71955026356962,0.496235646651272));
#7238=CARTESIAN_POINT('Ctrl Pts',(2.00835812169334,-0.0285906101811712,
0.873725226657167));
#7239=CARTESIAN_POINT('Ctrl Pts',(2.06221239278347,-0.639495616387645,0.513465547115104));
#7240=CARTESIAN_POINT('Ctrl Pts',(2.09485053865315,-0.737539630587503,0.132965811788644));
#7241=CARTESIAN_POINT('Ctrl Pts',(2.10627255930239,-0.737772979261817,-9.2067110508921E-5));
#7242=CARTESIAN_POINT('Origin',(-0.572772559302386,0.,0.));
#7243=CARTESIAN_POINT('',(1.22722744069761,-0.738274288005887,-0.000564985451368562));
#7244=CARTESIAN_POINT('',(1.30627255930239,-0.740190996501743,-0.000140724907590206));
#7245=CARTESIAN_POINT('',(-0.572772559302386,-0.739,-5.47916578054271E-15));
#7246=CARTESIAN_POINT('Ctrl Pts',(1.22722744069761,-0.738274288005887,-0.000564985451368596));
#7247=CARTESIAN_POINT('Ctrl Pts',(1.23440908921262,-0.738865989704968,-0.0841133359573396));
#7248=CARTESIAN_POINT('Ctrl Pts',(1.26280686294807,-0.687148195366904,-0.413770540317463));
#7249=CARTESIAN_POINT('Ctrl Pts',(1.31242076190396,-0.201475781147527,-0.850577571991093));
#7250=CARTESIAN_POINT('Ctrl Pts',(1.37606913756531,0.606744109840312,-0.629234775441834));
#7251=CARTESIAN_POINT('Ctrl Pts',(1.43971751322663,0.857344462334542,0.170397511755603));
#7252=CARTESIAN_POINT('Ctrl Pts',(1.50336588888797,0.32001443730518,0.813428097254852));
#7253=CARTESIAN_POINT('Ctrl Pts',(1.56586919804495,-0.496462244332193,0.710770306505323));
#7254=CARTESIAN_POINT('Ctrl Pts',(1.60715638198151,-0.739135297566226,0.231753267197539));
#7255=CARTESIAN_POINT('Ctrl Pts',(1.62722744069761,-0.740127216117252,-0.000243252607449037));
#7256=CARTESIAN_POINT('Ctrl Pts',(1.30627255930239,-0.740190996501743,-0.000140724907590199));
#7257=CARTESIAN_POINT('Ctrl Pts',(1.30692370267449,-0.740210604865509,-0.00766540411704673));
#7258=CARTESIAN_POINT('Ctrl Pts',(1.32879097126704,-0.736692111833655,-0.260346995818802));
#7259=CARTESIAN_POINT('Ctrl Pts',(1.37187436508003,-0.449657344341168,-0.749588466564275));
#7260=CARTESIAN_POINT('Ctrl Pts',(1.43552274074136,0.387638617164456,-0.783461202618526));
#7261=CARTESIAN_POINT('Ctrl Pts',(1.49917111640269,0.86868123199142,-0.0973041288729582));
#7262=CARTESIAN_POINT('Ctrl Pts',(1.56281949206402,0.551373824608492,0.678277263416331));
#7263=CARTESIAN_POINT('Ctrl Pts',(1.62646786772535,-0.272664316773187,0.830500694029215));
#7264=CARTESIAN_POINT('Ctrl Pts',(1.67428555680481,-0.703487412979108,0.371437303241661));
#7265=CARTESIAN_POINT('Ctrl Pts',(1.70088712066382,-0.739409808067928,0.0632113433965318));
#7266=CARTESIAN_POINT('Ctrl Pts',(1.70627255930239,-0.738843016432019,0.000681709321951364));
#7267=CARTESIAN_POINT('Origin',(-0.572772559302386,0.,0.));
#7268=CARTESIAN_POINT('',(0.827227440697613,-0.738071967478162,0.000461637341666832));
#7269=CARTESIAN_POINT('',(0.906272559302387,-0.738416445285999,-0.000613754558977386));
#7270=CARTESIAN_POINT('',(-0.572772559302386,-0.739,-5.47916578054271E-15));
#7271=CARTESIAN_POINT('Ctrl Pts',(0.827227440697613,-0.738071967478162,
0.000461637341666824));
#7272=CARTESIAN_POINT('Ctrl Pts',(0.840445671223291,-0.73719920677448,-0.153419961415631));
#7273=CARTESIAN_POINT('Ctrl Pts',(0.874880026969413,-0.61504271873664,-0.555561719131355));
#7274=CARTESIAN_POINT('Ctrl Pts',(0.93053050793598,0.0453327389257982,-0.872936419502457));
#7275=CARTESIAN_POINT('Ctrl Pts',(0.99417888359731,0.758952072968206,-0.433666741182324));
#7276=CARTESIAN_POINT('Ctrl Pts',(1.05782725925864,0.775067556196549,0.404160056571117));
#7277=CARTESIAN_POINT('Ctrl Pts',(1.12147563491997,0.0788680065218695,0.870548302528163));
#7278=CARTESIAN_POINT('Ctrl Pts',(1.1779423620663,-0.603081147802284,0.574521731828544));
#7279=CARTESIAN_POINT('Ctrl Pts',(1.21319296399218,-0.737117976374239,0.162706354896649));
#7280=CARTESIAN_POINT('Ctrl Pts',(1.22722744069761,-0.738274288005887,-0.000564985451368596));
#7281=CARTESIAN_POINT('Ctrl Pts',(0.906272559302387,-0.738416445285999,
-0.000613754558977378));
#7282=CARTESIAN_POINT('Ctrl Pts',(0.912960284685159,-0.739022836930718,
-0.0783783249613751));
#7283=CARTESIAN_POINT('Ctrl Pts',(0.940864135288376,-0.691859526234811,
-0.402126213356302));
#7284=CARTESIAN_POINT('Ctrl Pts',(0.989984111112038,-0.221217080729997,
-0.845658086769963));
#7285=CARTESIAN_POINT('Ctrl Pts',(1.05363248677337,0.591935303657854,-0.643185448607059));
#7286=CARTESIAN_POINT('Ctrl Pts',(1.1172808624347,0.861078022520812,0.15039794758511));
#7287=CARTESIAN_POINT('Ctrl Pts',(1.18092923809603,0.33885910720287,0.805760068695353));
#7288=CARTESIAN_POINT('Ctrl Pts',(1.24392647038526,-0.486254985425757,0.721471155828013));
#7289=CARTESIAN_POINT('Ctrl Pts',(1.28570757745405,-0.739571707936107,0.237510302480507));
#7290=CARTESIAN_POINT('Ctrl Pts',(1.30627255930239,-0.740190996501743,-0.000140724907590199));
#7291=CARTESIAN_POINT('Origin',(-0.572772559302386,0.,0.));
#7292=CARTESIAN_POINT('',(0.427227440697614,-0.739952215624597,0.000448480265853964));
#7293=CARTESIAN_POINT('',(0.506272559302387,-0.737970603191613,0.000391387174775056));
#7294=CARTESIAN_POINT('',(-0.572772559302386,-0.739,-5.47916578054271E-15));
#7295=CARTESIAN_POINT('Ctrl Pts',(0.427227440697614,-0.739952215624596,
0.000448480265853929));
#7296=CARTESIAN_POINT('Ctrl Pts',(0.446482253233962,-0.738507378828591,
-0.222229934060904));
#7297=CARTESIAN_POINT('Ctrl Pts',(0.486953190990754,-0.512839059320208,
-0.692987053973792));
#7298=CARTESIAN_POINT('Ctrl Pts',(0.54864025396799,0.288505105027068,-0.825086052852563));
#7299=CARTESIAN_POINT('Ctrl Pts',(0.612288629629321,0.850153462314954,-0.203265356679994));
#7300=CARTESIAN_POINT('Ctrl Pts',(0.675937005290653,0.630494869034967,0.605449773366773));
#7301=CARTESIAN_POINT('Ctrl Pts',(0.739585380951984,-0.168618773116491,
0.857689439427387));
#7302=CARTESIAN_POINT('Ctrl Pts',(0.790015526087638,-0.678988757841016,
0.433016557285913));
#7303=CARTESIAN_POINT('Ctrl Pts',(0.819229546002848,-0.738600044832254,
0.0935700772294608));
#7304=CARTESIAN_POINT('Ctrl Pts',(0.827227440697613,-0.738071967478162,
0.000461637341666824));
#7305=CARTESIAN_POINT('Ctrl Pts',(0.506272559302387,-0.737970603191613,
0.000391387174775012));
#7306=CARTESIAN_POINT('Ctrl Pts',(0.51899686669583,-0.737274229035035,-0.147792354816542));
#7307=CARTESIAN_POINT('Ctrl Pts',(0.552937299309717,-0.622015155205619,
-0.544057942892273));
#7308=CARTESIAN_POINT('Ctrl Pts',(0.608093857144047,0.0250062607190412,
-0.873749542443373));
#7309=CARTESIAN_POINT('Ctrl Pts',(0.671742232805379,0.748652522139804,-0.451215665674743));
#7310=CARTESIAN_POINT('Ctrl Pts',(0.73539060846671,0.784264444309691,0.386013618692408));
#7311=CARTESIAN_POINT('Ctrl Pts',(0.799038984128041,0.0991070357816886,
0.868476214982029));
#7312=CARTESIAN_POINT('Ctrl Pts',(0.855999634406602,-0.595570363064826,
0.585952374541452));
#7313=CARTESIAN_POINT('Ctrl Pts',(0.891744159464716,-0.7370991214175,0.16832182627709));
#7314=CARTESIAN_POINT('Ctrl Pts',(0.906272559302387,-0.738416445285999,
-0.000613754558977378));
#7315=CARTESIAN_POINT('Origin',(2.3266,2.39206768658147E-16,-5.43753587379397E-17));
#7316=CARTESIAN_POINT('',(2.3266,-0.855344277194458,-0.450546035351206));
#7317=CARTESIAN_POINT('Ctrl Pts',(2.3266,0.00705185163866655,0.740219785066309));
#7318=CARTESIAN_POINT('Ctrl Pts',(2.3266,-0.0091816416561815,0.742895096882004));
#7319=CARTESIAN_POINT('Ctrl Pts',(2.3266,-0.0254819710138712,0.744984144680738));
#7320=CARTESIAN_POINT('Ctrl Pts',(2.3266,-0.0418213189100594,0.746474642718444));
#7321=CARTESIAN_POINT('Ctrl Pts',(2.3266,-0.0752275148083482,0.749522002365228));
#7322=CARTESIAN_POINT('Ctrl Pts',(2.3266,-0.108795641758076,0.75007069080123));
#7323=CARTESIAN_POINT('Ctrl Pts',(2.3266,-0.142321448506824,0.748288394145316));
#7324=CARTESIAN_POINT('Ctrl Pts',(2.3266,-0.159005045099053,0.747401461919111));
#7325=CARTESIAN_POINT('Ctrl Pts',(2.3266,-0.175678490901637,0.745936553914972));
#7326=CARTESIAN_POINT('Ctrl Pts',(2.3266,-0.192318008684797,0.74391008090649));
#7327=CARTESIAN_POINT('Ctrl Pts',(2.3266,-0.20132065718867,0.74281367748689));
#7328=CARTESIAN_POINT('Ctrl Pts',(2.3266,-0.210304455697944,0.741553895478701));
#7329=CARTESIAN_POINT('Ctrl Pts',(2.3266,-0.219262804535322,0.740134541391542));
#7330=CARTESIAN_POINT('Ctrl Pts',(2.3266,-0.254598126832081,0.734536039364728));
#7331=CARTESIAN_POINT('Ctrl Pts',(2.3266,-0.289549801717428,0.72645730926244));
#7332=CARTESIAN_POINT('Ctrl Pts',(2.3266,-0.323887860257361,0.716079004587159));
#7333=CARTESIAN_POINT('Ctrl Pts',(2.3266,-0.338421060949871,0.711686502765355));
#7334=CARTESIAN_POINT('Ctrl Pts',(2.3266,-0.352844521793266,0.706881436906426));
#7335=CARTESIAN_POINT('Ctrl Pts',(2.3266,-0.36714126863909,0.701674762529288));
#7336=CARTESIAN_POINT('Ctrl Pts',(2.3266,-0.376760163394388,0.698171696174481));
#7337=CARTESIAN_POINT('Ctrl Pts',(2.3266,-0.386321702824635,0.694486802926217));
#7338=CARTESIAN_POINT('Ctrl Pts',(2.3266,-0.395820709108693,0.690623021799272));
#7339=CARTESIAN_POINT('Ctrl Pts',(2.3266,-0.403344093306561,0.687562837501546));
#7340=CARTESIAN_POINT('Ctrl Pts',(2.3266,-0.410819442882381,0.684394007476334));
#7341=CARTESIAN_POINT('Ctrl Pts',(2.3266,-0.418243797843197,0.681118946191534));
#7342=CARTESIAN_POINT('Ctrl Pts',(2.3266,-0.452853461534587,0.665851792313006));
#7343=CARTESIAN_POINT('Ctrl Pts',(2.3266,-0.486357659396555,0.648279158997269));
#7344=CARTESIAN_POINT('Ctrl Pts',(2.3266,-0.518509938036373,0.628592801474918));
#7345=CARTESIAN_POINT('Ctrl Pts',(2.3266,-0.550872267895178,0.608777832744591));
#7346=CARTESIAN_POINT('Ctrl Pts',(2.3266,-0.58186630614572,0.586821105901194));
#7347=CARTESIAN_POINT('Ctrl Pts',(2.3266,-0.611237088993447,0.562865246568347));
#7348=CARTESIAN_POINT('Ctrl Pts',(2.3266,-0.626354028635055,0.550535330764774));
#7349=CARTESIAN_POINT('Ctrl Pts',(2.3266,-0.641040769620426,0.53767500060788));
#7350=CARTESIAN_POINT('Ctrl Pts',(2.3266,-0.6552603442492,0.524298749950964));
#7351=CARTESIAN_POINT('Ctrl Pts',(2.3266,-0.660929329845617,0.518965976342203));
#7352=CARTESIAN_POINT('Ctrl Pts',(2.3266,-0.666523772205263,0.513551232266967));
#7353=CARTESIAN_POINT('Ctrl Pts',(2.3266,-0.67203149961292,0.508065585358026));
#7354=CARTESIAN_POINT('Ctrl Pts',(2.3266,-0.699029329476628,0.481175989890019));
#7355=CARTESIAN_POINT('Ctrl Pts',(2.3266,-0.72400691357688,0.452528609055507));
#7356=CARTESIAN_POINT('Ctrl Pts',(2.3266,-0.746728020736309,0.422283976342188));
#7357=CARTESIAN_POINT('Ctrl Pts',(2.3266,-0.769504982910754,0.391964993624598));
#7358=CARTESIAN_POINT('Ctrl Pts',(2.3266,-0.790016116737887,0.360040749577662));
#7359=CARTESIAN_POINT('Ctrl Pts',(2.3266,-0.808289814214594,0.326779688833403));
#7360=CARTESIAN_POINT('Ctrl Pts',(2.3266,-0.81696709711708,0.310985642002837));
#7361=CARTESIAN_POINT('Ctrl Pts',(2.3266,-0.825139367604472,0.294889551675988));
#7362=CARTESIAN_POINT('Ctrl Pts',(2.3266,-0.832806738358023,0.278517287953485));
#7363=CARTESIAN_POINT('Ctrl Pts',(2.3266,-0.837430380466189,0.268644348403992));
#7364=CARTESIAN_POINT('Ctrl Pts',(2.3266,-0.841870381472551,0.258670948237785));
#7365=CARTESIAN_POINT('Ctrl Pts',(2.3266,-0.846126407283495,0.248602508196632));
#7366=CARTESIAN_POINT('Ctrl Pts',(2.3266,-0.849263221090139,0.241181777417403));
#7367=CARTESIAN_POINT('Ctrl Pts',(2.3266,-0.852296360098048,0.233718192729926));
#7368=CARTESIAN_POINT('Ctrl Pts',(2.3266,-0.855225532626083,0.226216366154033));
#7369=CARTESIAN_POINT('Ctrl Pts',(2.3266,-0.869632326082018,0.189319507062694));
#7370=CARTESIAN_POINT('Ctrl Pts',(2.3266,-0.881533437703762,0.151485642669957));
#7371=CARTESIAN_POINT('Ctrl Pts',(2.3266,-0.890969066035468,0.113010070419481));
#7372=CARTESIAN_POINT('Ctrl Pts',(2.3266,-0.900622821965197,0.0736450413291914));
#7373=CARTESIAN_POINT('Ctrl Pts',(2.3266,-0.907696290859194,0.0336073077901501));
#7374=CARTESIAN_POINT('Ctrl Pts',(2.3266,-0.912190086870429,-0.00682105459462326));
#7375=CARTESIAN_POINT('Ctrl Pts',(2.3266,-0.914349459355949,-0.0262478138756487));
#7376=CARTESIAN_POINT('Ctrl Pts',(2.3266,-0.915912511260161,-0.0457651761268934));
#7377=CARTESIAN_POINT('Ctrl Pts',(2.3266,-0.916875413994828,-0.0653434748872564));
#7378=CARTESIAN_POINT('Ctrl Pts',(2.3266,-0.917299664358875,-0.0739695801806303));
#7379=CARTESIAN_POINT('Ctrl Pts',(2.3266,-0.917607376849151,-0.0826075237982675));
#7380=CARTESIAN_POINT('Ctrl Pts',(2.3266,-0.917798058061557,-0.0912548003913321));
#7381=CARTESIAN_POINT('Ctrl Pts',(2.3266,-0.917979847998161,-0.09949886305392));
#7382=CARTESIAN_POINT('Ctrl Pts',(2.3266,-0.918055035202284,-0.107741728314853));
#7383=CARTESIAN_POINT('Ctrl Pts',(2.3266,-0.918023912658678,-0.115979255927813));
#7384=CARTESIAN_POINT('Ctrl Pts',(2.3266,-0.917864023310433,-0.15829883423272));
#7385=CARTESIAN_POINT('Ctrl Pts',(2.3266,-0.91490237027171,-0.200490667473989));
#7386=CARTESIAN_POINT('Ctrl Pts',(2.3266,-0.909156732986574,-0.242248418365806));
#7387=CARTESIAN_POINT('Ctrl Pts',(2.3266,-0.903451049303708,-0.283715797191301));
#7388=CARTESIAN_POINT('Ctrl Pts',(2.3266,-0.895000225390717,-0.324756379279632));
#7389=CARTESIAN_POINT('Ctrl Pts',(2.3266,-0.883773539295331,-0.365084529739219));
#7390=CARTESIAN_POINT('Ctrl Pts',(2.3266,-0.875731688688448,-0.39397221382448));
#7391=CARTESIAN_POINT('Ctrl Pts',(2.3266,-0.866264537064502,-0.422494697859053));
#7392=CARTESIAN_POINT('Ctrl Pts',(2.3266,-0.855344277194458,-0.450546035351206));
#7393=CARTESIAN_POINT('',(2.3266,-0.96675,-1.1839272930757E-16));
#7394=CARTESIAN_POINT('Origin',(2.3266,0.,0.));
#7395=CARTESIAN_POINT('',(2.3266,-0.168638537403571,-0.953577585643768));
#7396=CARTESIAN_POINT('Origin',(2.3266,0.,0.));
#7397=CARTESIAN_POINT('Ctrl Pts',(2.3266,-0.16863827771112,-0.953592946438969));
#7398=CARTESIAN_POINT('Ctrl Pts',(2.3266,-0.147465654530663,-0.954986799957863));
#7399=CARTESIAN_POINT('Ctrl Pts',(2.3266,-0.126272781527092,-0.955629173556653));
#7400=CARTESIAN_POINT('Ctrl Pts',(2.3266,-0.10508809158694,-0.955496709949245));
#7401=CARTESIAN_POINT('Ctrl Pts',(2.3266,-0.0672410987773937,-0.955260060311641));
#7402=CARTESIAN_POINT('Ctrl Pts',(2.3266,-0.0294193568307657,-0.952552042729772));
#7403=CARTESIAN_POINT('Ctrl Pts',(2.3266,0.00817672626721474,-0.947478640546724));
#7404=CARTESIAN_POINT('Ctrl Pts',(2.3266,0.029679781676428,-0.944576911449813));
#7405=CARTESIAN_POINT('Ctrl Pts',(2.3266,0.0511088134843331,-0.940900810877595));
#7406=CARTESIAN_POINT('Ctrl Pts',(2.3266,0.0724238415269682,-0.936466009340783));
#7407=CARTESIAN_POINT('Ctrl Pts',(2.3266,0.0839551864399211,-0.934066799448158));
#7408=CARTESIAN_POINT('Ctrl Pts',(2.3266,0.0954546673735591,-0.931444891816811));
#7409=CARTESIAN_POINT('Ctrl Pts',(2.3266,0.106895029296963,-0.928608210414757));
#7410=CARTESIAN_POINT('Ctrl Pts',(2.3266,0.147435171064247,-0.918556127538547));
#7411=CARTESIAN_POINT('Ctrl Pts',(2.3266,0.187295630759207,-0.905798999992378));
#7412=CARTESIAN_POINT('Ctrl Pts',(2.3266,0.226199649503474,-0.890473975822821));
#7413=CARTESIAN_POINT('Ctrl Pts',(2.3266,0.248473621616919,-0.881699839576527));
#7414=CARTESIAN_POINT('Ctrl Pts',(2.3266,0.270433587385743,-0.872083121950981));
#7415=CARTESIAN_POINT('Ctrl Pts',(2.3266,0.292022276599161,-0.861643953482181));
#7416=CARTESIAN_POINT('Ctrl Pts',(2.3266,0.300263240856417,-0.857659051324555));
#7417=CARTESIAN_POINT('Ctrl Pts',(2.3266,0.308450056697937,-0.853554269336753));
#7418=CARTESIAN_POINT('Ctrl Pts',(2.3266,0.31657934911869,-0.849330600533629));
#7419=CARTESIAN_POINT('Ctrl Pts',(2.3266,0.323957422231335,-0.845497236494036));
#7420=CARTESIAN_POINT('Ctrl Pts',(2.3266,0.331284238554771,-0.84156787828759));
#7421=CARTESIAN_POINT('Ctrl Pts',(2.3266,0.338550765117836,-0.837547399129169));
#7422=CARTESIAN_POINT('Ctrl Pts',(2.3266,0.373670084967107,-0.818116314375472));
#7423=CARTESIAN_POINT('Ctrl Pts',(2.3266,0.407433256551024,-0.796534237223156));
#7424=CARTESIAN_POINT('Ctrl Pts',(2.3266,0.439589982929631,-0.772920787990529));
#7425=CARTESIAN_POINT('Ctrl Pts',(2.3266,0.470995194774116,-0.749859193759874));
#7426=CARTESIAN_POINT('Ctrl Pts',(2.3266,0.500868881519513,-0.724859244899778));
#7427=CARTESIAN_POINT('Ctrl Pts',(2.3266,0.528937790278082,-0.698005501260112));
#7428=CARTESIAN_POINT('Ctrl Pts',(2.3266,0.541876813655034,-0.685626636812585));
#7429=CARTESIAN_POINT('Ctrl Pts',(2.3266,0.554431696369729,-0.672853541668634));
#7430=CARTESIAN_POINT('Ctrl Pts',(2.3266,0.566572088464898,-0.659693216914725));
#7431=CARTESIAN_POINT('Ctrl Pts',(2.3266,0.572732958972858,-0.653014762379159));
#7432=CARTESIAN_POINT('Ctrl Pts',(2.3266,0.578787048944214,-0.646236576282453));
#7433=CARTESIAN_POINT('Ctrl Pts',(2.3266,0.584730139804016,-0.639359518753095));
#7434=CARTESIAN_POINT('Ctrl Pts',(2.3266,0.589432586433977,-0.633918074769507));
#7435=CARTESIAN_POINT('Ctrl Pts',(2.3266,0.594063483497632,-0.628416996597973));
#7436=CARTESIAN_POINT('Ctrl Pts',(2.3266,0.598615889829617,-0.622863232110901));
#7437=CARTESIAN_POINT('Ctrl Pts',(2.3266,0.621523554501612,-0.594916742878777));
#7438=CARTESIAN_POINT('Ctrl Pts',(2.3266,0.642487414808634,-0.565591201764512));
#7439=CARTESIAN_POINT('Ctrl Pts',(2.3266,0.661292448179919,-0.534963557358698));
#7440=CARTESIAN_POINT('Ctrl Pts',(2.3266,0.678661125771888,-0.506675296945486));
#7441=CARTESIAN_POINT('Ctrl Pts',(2.3266,0.69418763594692,-0.477275294544982));
#7442=CARTESIAN_POINT('Ctrl Pts',(2.3266,0.707850085022545,-0.446949904939736));
#7443=CARTESIAN_POINT('Ctrl Pts',(2.3266,0.721108132135827,-0.417522132372059));
#7444=CARTESIAN_POINT('Ctrl Pts',(2.3266,0.732610655706484,-0.387222336042198));
#7445=CARTESIAN_POINT('Ctrl Pts',(2.3266,0.742311682314211,-0.356223725233837));
#7446=CARTESIAN_POINT('Ctrl Pts',(2.3266,0.74472416850348,-0.348514879202826));
#7447=CARTESIAN_POINT('Ctrl Pts',(2.3266,0.747022672915413,-0.340770513432795));
#7448=CARTESIAN_POINT('Ctrl Pts',(2.3266,0.749205684083773,-0.332998578461517));
#7449=CARTESIAN_POINT('Ctrl Pts',(2.3266,0.759292423406657,-0.297087867959487));
#7450=CARTESIAN_POINT('Ctrl Pts',(2.3266,0.766928667050838,-0.260553256960538));
#7451=CARTESIAN_POINT('Ctrl Pts',(2.3266,0.772094075526193,-0.223665502925765));
#7452=CARTESIAN_POINT('Ctrl Pts',(2.3266,0.777195092102294,-0.187237591041495));
#7453=CARTESIAN_POINT('Ctrl Pts',(2.3266,0.779886220465533,-0.15046400931105));
#7454=CARTESIAN_POINT('Ctrl Pts',(2.3266,0.780099171435814,-0.113617901149199));
#7455=CARTESIAN_POINT('Ctrl Pts',(2.3266,0.780199873465589,-0.0961938064089577));
#7456=CARTESIAN_POINT('Ctrl Pts',(2.3266,0.779745712369878,-0.0787537915307566));
#7457=CARTESIAN_POINT('Ctrl Pts',(2.3266,0.778725867603093,-0.0613289396111699));
#7458=CARTESIAN_POINT('Ctrl Pts',(2.3266,0.778171162891524,-0.0518513722666234));
#7459=CARTESIAN_POINT('Ctrl Pts',(2.3266,0.777448585933176,-0.0423751470953692));
#7460=CARTESIAN_POINT('Ctrl Pts',(2.3266,0.77655899786828,-0.0329302576238707));
#7461=CARTESIAN_POINT('Ctrl Pts',(2.3266,0.7732468432591,0.00223538300316667));
#7462=CARTESIAN_POINT('Ctrl Pts',(2.3266,0.767620707505793,0.0370380579314474));
#7463=CARTESIAN_POINT('Ctrl Pts',(2.3266,0.759636976250263,0.0712350618987401));
#7464=CARTESIAN_POINT('Ctrl Pts',(2.3266,0.751943629281566,0.104188252379458));
#7465=CARTESIAN_POINT('Ctrl Pts',(2.3266,0.742060610076505,0.136579845357312));
#7466=CARTESIAN_POINT('Ctrl Pts',(2.3266,0.729909685892531,0.168165888140475));
#7467=CARTESIAN_POINT('Ctrl Pts',(2.3266,0.721569647399475,0.189845622839368));
#7468=CARTESIAN_POINT('Ctrl Pts',(2.3266,0.712160386241925,0.211145303211162));
#7469=CARTESIAN_POINT('Ctrl Pts',(2.3266,0.70164690293637,0.231975480600428));
#7470=CARTESIAN_POINT('Ctrl Pts',(0.0352584761920629,-0.324968229607101,
0.663714283216827));
#7471=CARTESIAN_POINT('Ctrl Pts',(0.0564746014125068,-0.546159055819686,
0.555414683498625));
#7472=CARTESIAN_POINT('Ctrl Pts',(0.0989068518533947,-0.867866968611021,
0.10213065993041));
#7473=CARTESIAN_POINT('Ctrl Pts',(0.162555227514726,-0.554389096255145,
-0.676579895838483));
#7474=CARTESIAN_POINT('Ctrl Pts',(0.226203603176058,0.269321839759082,-0.831315270808783));
#7475=CARTESIAN_POINT('Ctrl Pts',(0.289851978837389,0.845141343193606,-0.223133510528201));
#7476=CARTESIAN_POINT('Ctrl Pts',(0.35350035449872,0.644441981350638,0.590684118087253));
#7477=CARTESIAN_POINT('Ctrl Pts',(0.417148730160053,-0.148625865295904,
0.86134357313186));
#7478=CARTESIAN_POINT('Ctrl Pts',(0.480797105821384,-0.805046913683514,
0.340554311735867));
#7479=CARTESIAN_POINT('Ctrl Pts',(0.544445481482716,-0.721629565711504,
-0.493299137187071));
#7480=CARTESIAN_POINT('Ctrl Pts',(0.608093857144047,0.0250062607190412,
-0.873749542443373));
#7481=CARTESIAN_POINT('Ctrl Pts',(0.671742232805379,0.748652522139804,-0.451215665674743));
#7482=CARTESIAN_POINT('Ctrl Pts',(0.73539060846671,0.784264444309691,0.386013618692408));
#7483=CARTESIAN_POINT('Ctrl Pts',(0.799038984128041,0.0991070357816886,
0.868476214982029));
#7484=CARTESIAN_POINT('Ctrl Pts',(0.862687359789374,-0.677132136857513,
0.552781372284408));
#7485=CARTESIAN_POINT('Ctrl Pts',(0.926335735450704,-0.831063210972372,
-0.270941124405154));
#7486=CARTESIAN_POINT('Ctrl Pts',(0.989984111112038,-0.221217080729997,
-0.845658086769963));
#7487=CARTESIAN_POINT('Ctrl Pts',(1.05363248677337,0.591935303657854,-0.643185448607059));
#7488=CARTESIAN_POINT('Ctrl Pts',(1.1172808624347,0.861078022520812,0.15039794758511));
#7489=CARTESIAN_POINT('Ctrl Pts',(1.18092923809603,0.33885910720287,0.805760068695353));
#7490=CARTESIAN_POINT('Ctrl Pts',(1.24457761375736,-0.494783416804721,0.720599940300586));
#7491=CARTESIAN_POINT('Ctrl Pts',(1.30822598941869,-0.873702320661405,-0.0268175294771084));
#7492=CARTESIAN_POINT('Ctrl Pts',(1.37187436508003,-0.449657344341168,-0.749588466564275));
#7493=CARTESIAN_POINT('Ctrl Pts',(1.43552274074136,0.387638617164456,-0.783461202618526));
#7494=CARTESIAN_POINT('Ctrl Pts',(1.49917111640269,0.86868123199142,-0.0973041288729582));
#7495=CARTESIAN_POINT('Ctrl Pts',(1.56281949206402,0.551373824608492,0.678277263416331));
#7496=CARTESIAN_POINT('Ctrl Pts',(1.62646786772535,-0.272664316773187,0.830500694029215));
#7497=CARTESIAN_POINT('Ctrl Pts',(1.69011624338669,-0.846117170701959,0.219458217663196));
#7498=CARTESIAN_POINT('Ctrl Pts',(1.75376461904801,-0.64195232541919,-0.593262832043307));
#7499=CARTESIAN_POINT('Ctrl Pts',(1.81741299470935,0.152178910917555,-0.860775724524354));
#7500=CARTESIAN_POINT('Ctrl Pts',(1.88106137037068,0.806472809610774,-0.33716372852332));
#7501=CARTESIAN_POINT('Ctrl Pts',(1.94470974603201,0.71955026356962,0.496235646651272));
#7502=CARTESIAN_POINT('Ctrl Pts',(2.00835812169334,-0.0285906101811712,
0.873725226657167));
#7503=CARTESIAN_POINT('Ctrl Pts',(2.07200649735467,-0.750596693289163,0.447947605774497));
#7504=CARTESIAN_POINT('Ctrl Pts',(2.13565487301601,-0.782508756785437,-0.388972207754245));
#7505=CARTESIAN_POINT('Ctrl Pts',(2.19930324867733,-0.0957849414937873,
-0.86944400077431));
#7506=CARTESIAN_POINT('Ctrl Pts',(2.26295162433867,0.68001209321599,-0.548823559975255));
#7507=CARTESIAN_POINT('Ctrl Pts',(2.30538387477956,0.778955542380413,-0.00185685071207135));
#7508=CARTESIAN_POINT('Ctrl Pts',(2.3266,0.701646902936369,0.231975480600434));
#7509=CARTESIAN_POINT('Ctrl Pts',(0.079088984128042,-0.358351862576436,
0.731896930038042));
#7510=CARTESIAN_POINT('Ctrl Pts',(0.100305109348486,-0.60226538191934,0.612471830168365));
#7511=CARTESIAN_POINT('Ctrl Pts',(0.142737359789373,-0.95702199887767,0.11262243160346));
#7512=CARTESIAN_POINT('Ctrl Pts',(0.206385735450706,-0.611340885462232,
-0.746084213058696));
#7513=CARTESIAN_POINT('Ctrl Pts',(0.270034111112036,0.296988979589994,-0.916715384893899));
#7514=CARTESIAN_POINT('Ctrl Pts',(0.333682486773368,0.931961794665117,-0.246055773506459));
#7515=CARTESIAN_POINT('Ctrl Pts',(0.3973308624347,0.710644805551184,0.651364455432481));
#7516=CARTESIAN_POINT('Ctrl Pts',(0.460979238096031,-0.163894038873325,
0.949828462072222));
#7517=CARTESIAN_POINT('Ctrl Pts',(0.524627613757363,-0.887748507996287,
0.375539085979369));
#7518=CARTESIAN_POINT('Ctrl Pts',(0.588275989418695,-0.795761786546325,
-0.543975221307212));
#7519=CARTESIAN_POINT('Ctrl Pts',(0.651924365080026,0.027575126699538,-0.963508883125141));
#7520=CARTESIAN_POINT('Ctrl Pts',(0.715572740741357,0.825560781913074,-0.497568560513454));
#7521=CARTESIAN_POINT('Ctrl Pts',(0.779221116402689,0.864831078135372,0.425668378122807));
#7522=CARTESIAN_POINT('Ctrl Pts',(0.842869492064021,0.109288193832785,0.957693832466087));
#7523=CARTESIAN_POINT('Ctrl Pts',(0.906517867725353,-0.746693185197295,
0.609568001755664));
#7524=CARTESIAN_POINT('Ctrl Pts',(0.970166243386683,-0.916437431224496,
-0.298774611587505));
#7525=CARTESIAN_POINT('Ctrl Pts',(1.03381461904802,-0.24394247095835,-0.932531622747347));
#7526=CARTESIAN_POINT('Ctrl Pts',(1.09746299470935,0.652744173936643,-0.709259190564775));
#7527=CARTESIAN_POINT('Ctrl Pts',(1.16111137037068,0.949535631735567,0.165848165249749));
#7528=CARTESIAN_POINT('Ctrl Pts',(1.22475974603201,0.373669734927479,0.888534924647256));
#7529=CARTESIAN_POINT('Ctrl Pts',(1.28840812169334,-0.545611979356493,0.794626388836201));
#7530=CARTESIAN_POINT('Ctrl Pts',(1.35205649735467,-0.963456810300842,-0.0295724651281722));
#7531=CARTESIAN_POINT('Ctrl Pts',(1.415704873016,-0.495850154523263,-0.826592874890849));
#7532=CARTESIAN_POINT('Ctrl Pts',(1.47935324867734,0.427460310921427,-0.86394532029844));
#7533=CARTESIAN_POINT('Ctrl Pts',(1.54300162433867,0.957919910649988,-0.107300076257179));
#7534=CARTESIAN_POINT('Ctrl Pts',(1.60665,0.608015858237083,0.747955949362685));
#7535=CARTESIAN_POINT('Ctrl Pts',(1.67029837566133,-0.300674825634303,0.915817127527255));
#7536=CARTESIAN_POINT('Ctrl Pts',(1.73394675132266,-0.933037867872626,0.242002921800675));
#7537=CARTESIAN_POINT('Ctrl Pts',(1.79759512698399,-0.70789938997229,-0.654208077870038));
#7538=CARTESIAN_POINT('Ctrl Pts',(1.86124350264533,0.167812085009332,-0.949202278994549));
#7539=CARTESIAN_POINT('Ctrl Pts',(1.92489187830666,0.88932088466213,-0.371800191839147));
#7540=CARTESIAN_POINT('Ctrl Pts',(1.98854025396799,0.793468879955719,0.547213395196526));
#7541=CARTESIAN_POINT('Ctrl Pts',(2.05218862962932,-0.0315276924855277,
0.963482069404649));
#7542=CARTESIAN_POINT('Ctrl Pts',(2.11583700529065,-0.827704675651187,0.493964776372216));
#7543=CARTESIAN_POINT('Ctrl Pts',(2.17948538095199,-0.862895030740277,-0.428930899822819));
#7544=CARTESIAN_POINT('Ctrl Pts',(2.24313375661331,-0.105624824409986,-0.958761037840773));
#7545=CARTESIAN_POINT('Ctrl Pts',(2.30678213227465,0.749868996341809,-0.605203607690351));
#7546=CARTESIAN_POINT('Ctrl Pts',(2.34921438271553,0.858976798481964,-0.0020476029672245));
#7547=CARTESIAN_POINT('Ctrl Pts',(2.37043050793598,0.773726326546544,0.255806069552507));
#7548=CARTESIAN_POINT('Ctrl Pts',(0.122919492064021,-0.391735495545771,
0.800079576859257));
#7549=CARTESIAN_POINT('Ctrl Pts',(0.144135617284465,-0.658371708018994,
0.669528976838104));
#7550=CARTESIAN_POINT('Ctrl Pts',(0.186567867725353,-1.04617702914432,0.123114203276511));
#7551=CARTESIAN_POINT('Ctrl Pts',(0.250216243386685,-0.668292674669318,
-0.81558853027891));
#7552=CARTESIAN_POINT('Ctrl Pts',(0.313864619048016,0.324656119420904,-1.00211549897901));
#7553=CARTESIAN_POINT('Ctrl Pts',(0.377512994709347,1.01878224613663,-0.268978036484718));
#7554=CARTESIAN_POINT('Ctrl Pts',(0.441161370370679,0.776847629751729,0.712044792777709));
#7555=CARTESIAN_POINT('Ctrl Pts',(0.50480974603201,-0.179162212450745,1.03831335101258));
#7556=CARTESIAN_POINT('Ctrl Pts',(0.568458121693342,-0.97045010230906,0.410523860222872));
#7557=CARTESIAN_POINT('Ctrl Pts',(0.632106497354674,-0.869894007381145,
-0.594651305427354));
#7558=CARTESIAN_POINT('Ctrl Pts',(0.695754873016005,0.0301439926800345,
-1.05326822380691));
#7559=CARTESIAN_POINT('Ctrl Pts',(0.759403248677337,0.902469041686343,-0.543921455352166));
#7560=CARTESIAN_POINT('Ctrl Pts',(0.823051624338668,0.945397711961052,0.465323137553205));
#7561=CARTESIAN_POINT('Ctrl Pts',(0.886699999999999,0.119469351883882,1.04691144995015));
#7562=CARTESIAN_POINT('Ctrl Pts',(0.950348375661332,-0.816254233537077,
0.666354631226919));
#7563=CARTESIAN_POINT('Ctrl Pts',(1.01399675132266,-1.00181165147662,-0.326608098769855));
#7564=CARTESIAN_POINT('Ctrl Pts',(1.077645126984,-0.266667861186703,-1.01940515872473));
#7565=CARTESIAN_POINT('Ctrl Pts',(1.14129350264533,0.713553044215432,-0.775332932522492));
#7566=CARTESIAN_POINT('Ctrl Pts',(1.20494187830666,1.03799324095032,0.18129838291439));
#7567=CARTESIAN_POINT('Ctrl Pts',(1.26859025396799,0.408480362652086,0.971309780599157));
#7568=CARTESIAN_POINT('Ctrl Pts',(1.33223862962932,-0.596440541908263,0.868652837371817));
#7569=CARTESIAN_POINT('Ctrl Pts',(1.39588700529065,-1.05321129994028,-0.0323274007792368));
#7570=CARTESIAN_POINT('Ctrl Pts',(1.45953538095198,-0.542042964705357,-0.903597283217423));
#7571=CARTESIAN_POINT('Ctrl Pts',(1.52318375661332,0.467282004678397,-0.944429437978354));
#7572=CARTESIAN_POINT('Ctrl Pts',(1.58683213227465,1.04715858930856,-0.1172960236414));
#7573=CARTESIAN_POINT('Ctrl Pts',(1.65048050793598,0.664657891865674,0.81763463530904));
#7574=CARTESIAN_POINT('Ctrl Pts',(1.71412888359731,-0.328685334495418,1.00113356102529));
#7575=CARTESIAN_POINT('Ctrl Pts',(1.77777725925864,-1.01995856504329,0.264547625938156));
#7576=CARTESIAN_POINT('Ctrl Pts',(1.84142563491997,-0.773846454525389,-0.715153323696768));
#7577=CARTESIAN_POINT('Ctrl Pts',(1.9050740105813,0.183445259101111,-1.03762883346474));
#7578=CARTESIAN_POINT('Ctrl Pts',(1.96872238624264,0.972168959713482,-0.406436655154973));
#7579=CARTESIAN_POINT('Ctrl Pts',(2.03237076190397,0.86738749634182,0.598191143741779));
#7580=CARTESIAN_POINT('Ctrl Pts',(2.0960191375653,-0.0344647747898869,1.05323891215213));
#7581=CARTESIAN_POINT('Ctrl Pts',(2.15966751322663,-0.904812658013209,0.539981946969935));
#7582=CARTESIAN_POINT('Ctrl Pts',(2.22331588888796,-0.94328130469512,-0.468889591891392));
#7583=CARTESIAN_POINT('Ctrl Pts',(2.28696426454929,-0.115464707326183,-1.04807807490724));
#7584=CARTESIAN_POINT('Ctrl Pts',(2.35061264021063,0.819725899467628,-0.661583655405445));
#7585=CARTESIAN_POINT('Ctrl Pts',(2.39304489065151,0.938998054583516,-0.00223835522237897));
#7586=CARTESIAN_POINT('Ctrl Pts',(2.41426101587196,0.845805750156719,0.279636658504581));
#7587=CARTESIAN_POINT('Ctrl Pts',(0.16675,-0.425119128515106,0.868262223680471));
#7588=CARTESIAN_POINT('Ctrl Pts',(0.187966125220444,-0.714478034118648,
0.726586123507844));
#7589=CARTESIAN_POINT('Ctrl Pts',(0.230398375661332,-1.13533205941097,0.13360597494956));
#7590=CARTESIAN_POINT('Ctrl Pts',(0.294046751322664,-0.725244463876405,
-0.885092847499123));
#7591=CARTESIAN_POINT('Ctrl Pts',(0.357695126983995,0.352323259251816,-1.08751561306413));
#7592=CARTESIAN_POINT('Ctrl Pts',(0.421343502645326,1.10560269760814,-0.291900299462976));
#7593=CARTESIAN_POINT('Ctrl Pts',(0.484991878306658,0.843050453952274,0.772725130122938));
#7594=CARTESIAN_POINT('Ctrl Pts',(0.54864025396799,-0.194430386028165,1.12679823995294));
#7595=CARTESIAN_POINT('Ctrl Pts',(0.612288629629321,-1.05315169662183,0.445508634466375));
#7596=CARTESIAN_POINT('Ctrl Pts',(0.675937005290653,-0.944026228215964,
-0.645327389547496));
#7597=CARTESIAN_POINT('Ctrl Pts',(0.739585380951984,0.0327128586605295,
-1.14302756448867));
#7598=CARTESIAN_POINT('Ctrl Pts',(0.803233756613316,0.979377301459615,-0.590274350190879));
#7599=CARTESIAN_POINT('Ctrl Pts',(0.866882132274647,1.02596434578673,0.504977896983606));
#7600=CARTESIAN_POINT('Ctrl Pts',(0.930530507935979,0.129650509934979,1.1361290674342));
#7601=CARTESIAN_POINT('Ctrl Pts',(0.994178883597311,-0.885815281876861,
0.723141260698177));
#7602=CARTESIAN_POINT('Ctrl Pts',(1.05782725925864,-1.08718587172874,-0.354441585952207));
#7603=CARTESIAN_POINT('Ctrl Pts',(1.12147563491997,-0.289393251415056,-1.10627869470211));
#7604=CARTESIAN_POINT('Ctrl Pts',(1.1851240105813,0.774361914494221,-0.841406674480209));
#7605=CARTESIAN_POINT('Ctrl Pts',(1.24877238624264,1.12645085016508,0.19674860057903));
#7606=CARTESIAN_POINT('Ctrl Pts',(1.31242076190397,0.443290990376694,1.05408463655106));
#7607=CARTESIAN_POINT('Ctrl Pts',(1.3760691375653,-0.647269104460033,0.942679285907431));
#7608=CARTESIAN_POINT('Ctrl Pts',(1.43971751322663,-1.14296578957972,-0.0350823364303007));
#7609=CARTESIAN_POINT('Ctrl Pts',(1.50336588888796,-0.588235774887451,-0.980601691543996));
#7610=CARTESIAN_POINT('Ctrl Pts',(1.5670142645493,0.507103698435367,-1.02491355565827));
#7611=CARTESIAN_POINT('Ctrl Pts',(1.63066264021062,1.13639726796712,-0.127291971025621));
#7612=CARTESIAN_POINT('Ctrl Pts',(1.69431101587196,0.721299925494264,0.887313321255395));
#7613=CARTESIAN_POINT('Ctrl Pts',(1.75795939153329,-0.356695843356533,1.08644999452333));
#7614=CARTESIAN_POINT('Ctrl Pts',(1.82160776719462,-1.10687926221396,0.287092330075636));
#7615=CARTESIAN_POINT('Ctrl Pts',(1.88525614285595,-0.839793519078488,-0.776098569523499));
#7616=CARTESIAN_POINT('Ctrl Pts',(1.94890451851729,0.199078433192889,-1.12605538793494));
#7617=CARTESIAN_POINT('Ctrl Pts',(2.01255289417861,1.05501703476484,-0.441073118470799));
#7618=CARTESIAN_POINT('Ctrl Pts',(2.07620126983995,0.941306112727917,0.649168892287031));
#7619=CARTESIAN_POINT('Ctrl Pts',(2.13984964550128,-0.0374018570942429,
1.14299575489962));
#7620=CARTESIAN_POINT('Ctrl Pts',(2.20349802116261,-0.981920640375234,0.585999117567654));
#7621=CARTESIAN_POINT('Ctrl Pts',(2.26714639682394,-1.02366757864996,-0.508848283959966));
#7622=CARTESIAN_POINT('Ctrl Pts',(2.33079477248527,-0.125304590242383,-1.1373951119737));
#7623=CARTESIAN_POINT('Ctrl Pts',(2.39444314814661,0.889582802593447,-0.717963703120541));
#7624=CARTESIAN_POINT('Ctrl Pts',(2.43687539858749,1.01901931068507,-0.00242910747753216));
#7625=CARTESIAN_POINT('Ctrl Pts',(2.45809152380794,0.917885173766894,0.303467247456655));
#7626=CARTESIAN_POINT('Ctrl Pts',(2.23776408311032,-0.965144827742031,-0.000120440973035392));
#7627=CARTESIAN_POINT('Ctrl Pts',(2.24755818768153,-0.965406583880997,-0.149376556276826));
#7628=CARTESIAN_POINT('Ctrl Pts',(2.25735229225274,-0.932889906533184,-0.298535024733765));
#7629=CARTESIAN_POINT('Ctrl Pts',(2.26714639682394,-0.866982590869575,-0.431131521707652));
#7630=CARTESIAN_POINT('Ctrl Pts',(2.28696426454929,-0.733622521609705,-0.699433725218841));
#7631=CARTESIAN_POINT('Ctrl Pts',(2.30678213227465,-0.463549677312364,-0.899925512525171));
#7632=CARTESIAN_POINT('Ctrl Pts',(2.3266,-0.168638277711113,-0.95359294643897));
#7633=CARTESIAN_POINT('',(0.16675,-0.429877377952346,-0.601104350279397));
#7634=CARTESIAN_POINT('Ctrl Pts',(0.16675,-0.430804868963501,-0.60198184778573));
#7635=CARTESIAN_POINT('Ctrl Pts',(0.16675,-0.445493125509025,-0.594569785083027));
#7636=CARTESIAN_POINT('Ctrl Pts',(0.16675,-0.459889646383086,-0.586644826880307));
#7637=CARTESIAN_POINT('Ctrl Pts',(0.16675,-0.473964720489372,-0.57821345471323));
#7638=CARTESIAN_POINT('Ctrl Pts',(0.16675,-0.502741553314337,-0.56097530836282));
#7639=CARTESIAN_POINT('Ctrl Pts',(0.16675,-0.530175722996942,-0.541623677822874));
#7640=CARTESIAN_POINT('Ctrl Pts',(0.16675,-0.556201153620589,-0.520414434550179));
#7641=CARTESIAN_POINT('Ctrl Pts',(0.16675,-0.569152311242204,-0.50985997892437));
#7642=CARTESIAN_POINT('Ctrl Pts',(0.16675,-0.581754443541687,-0.498844719299822));
#7643=CARTESIAN_POINT('Ctrl Pts',(0.16675,-0.593998024650347,-0.48739593053637));
#7644=CARTESIAN_POINT('Ctrl Pts',(0.16675,-0.600622288153534,-0.481201681248652));
#7645=CARTESIAN_POINT('Ctrl Pts',(0.16675,-0.607134985115756,-0.47488659859674));
#7646=CARTESIAN_POINT('Ctrl Pts',(0.16675,-0.61353303015818,-0.468457648512547));
#7647=CARTESIAN_POINT('Ctrl Pts',(0.16675,-0.638769508932995,-0.443099267746505));
#7648=CARTESIAN_POINT('Ctrl Pts',(0.16675,-0.662233574464342,-0.41596401595051));
#7649=CARTESIAN_POINT('Ctrl Pts',(0.16675,-0.683846027178802,-0.387333403011322));
#7650=CARTESIAN_POINT('Ctrl Pts',(0.16675,-0.692993268657504,-0.375215799623217));
#7651=CARTESIAN_POINT('Ctrl Pts',(0.16675,-0.701808594899562,-0.362829709101333));
#7652=CARTESIAN_POINT('Ctrl Pts',(0.16675,-0.710284757451846,-0.350193988883425));
#7653=CARTESIAN_POINT('Ctrl Pts',(0.16675,-0.715987571926311,-0.341692598341481));
#7654=CARTESIAN_POINT('Ctrl Pts',(0.16675,-0.721536841075486,-0.333078179490395));
#7655=CARTESIAN_POINT('Ctrl Pts',(0.16675,-0.7269301162124,-0.324356159333427));
#7656=CARTESIAN_POINT('Ctrl Pts',(0.16675,-0.731201614784776,-0.317448279482511));
#7657=CARTESIAN_POINT('Ctrl Pts',(0.16675,-0.735370253785842,-0.310480981392049));
#7658=CARTESIAN_POINT('Ctrl Pts',(0.16675,-0.739435066871342,-0.30345795973618));
#7659=CARTESIAN_POINT('Ctrl Pts',(0.16675,-0.758383963144114,-0.270718813783024));
#7660=CARTESIAN_POINT('Ctrl Pts',(0.16675,-0.775080533888005,-0.23676957537437));
#7661=CARTESIAN_POINT('Ctrl Pts',(0.16675,-0.789438812866396,-0.20191044083355));
#7662=CARTESIAN_POINT('Ctrl Pts',(0.16675,-0.803890891927935,-0.166823577765984));
#7663=CARTESIAN_POINT('Ctrl Pts',(0.16675,-0.815974925978725,-0.130813832498557));
#7664=CARTESIAN_POINT('Ctrl Pts',(0.16675,-0.825569104336731,-0.0941467411674717));
#7665=CARTESIAN_POINT('Ctrl Pts',(0.16675,-0.830507164894443,-0.0752744301980837));
#7666=CARTESIAN_POINT('Ctrl Pts',(0.16675,-0.834785003923765,-0.056227423211327));
#7667=CARTESIAN_POINT('Ctrl Pts',(0.16675,-0.838381312156127,-0.0370392251201134));
#7668=CARTESIAN_POINT('Ctrl Pts',(0.16675,-0.839815065498442,-0.0293893960819031));
#7669=CARTESIAN_POINT('Ctrl Pts',(0.16675,-0.841140278900315,-0.0217173226060706));
#7670=CARTESIAN_POINT('Ctrl Pts',(0.16675,-0.842353648640237,-0.0140391205839416));
#7671=CARTESIAN_POINT('Ctrl Pts',(0.16675,-0.84830136567568,0.0235980245219733));
#7672=CARTESIAN_POINT('Ctrl Pts',(0.16675,-0.851580929224255,0.0614634969090231));
#7673=CARTESIAN_POINT('Ctrl Pts',(0.16675,-0.85209621782855,0.0992883442314791));
#7674=CARTESIAN_POINT('Ctrl Pts',(0.16675,-0.852612773449657,0.137206197137624));
#7675=CARTESIAN_POINT('Ctrl Pts',(0.16675,-0.850352775477891,0.175084379198237));
#7676=CARTESIAN_POINT('Ctrl Pts',(0.16675,-0.845497452406605,0.212722826928005));
#7677=CARTESIAN_POINT('Ctrl Pts',(0.16675,-0.843191897632869,0.230595479595049));
#7678=CARTESIAN_POINT('Ctrl Pts',(0.16675,-0.840300368383401,0.248414272293587));
#7679=CARTESIAN_POINT('Ctrl Pts',(0.16675,-0.836838210915746,0.266158377798457));
#7680=CARTESIAN_POINT('Ctrl Pts',(0.16675,-0.834750433503057,0.276858567789101));
#7681=CARTESIAN_POINT('Ctrl Pts',(0.16675,-0.8324551019924,0.287531601952822));
#7682=CARTESIAN_POINT('Ctrl Pts',(0.16675,-0.829955143091132,0.298172905292354));
#7683=CARTESIAN_POINT('Ctrl Pts',(0.16675,-0.828112598179905,0.30601586595348));
#7684=CARTESIAN_POINT('Ctrl Pts',(0.16675,-0.8261610517908,0.313832300947477));
#7685=CARTESIAN_POINT('Ctrl Pts',(0.16675,-0.824102988029633,0.321618313365642));
#7686=CARTESIAN_POINT('Ctrl Pts',(0.16675,-0.813980647604896,0.359912884085456));
#7687=CARTESIAN_POINT('Ctrl Pts',(0.16675,-0.801282102136966,0.39748663728072));
#7688=CARTESIAN_POINT('Ctrl Pts',(0.16675,-0.786213950326801,0.434124784279322));
#7689=CARTESIAN_POINT('Ctrl Pts',(0.16675,-0.770797461365757,0.471609911577817));
#7690=CARTESIAN_POINT('Ctrl Pts',(0.16675,-0.752900368761167,0.508116767940505));
#7691=CARTESIAN_POINT('Ctrl Pts',(0.16675,-0.73268950485522,0.543417900500982));
#7692=CARTESIAN_POINT('Ctrl Pts',(0.16675,-0.722977720127076,0.560380906223174));
#7693=CARTESIAN_POINT('Ctrl Pts',(0.16675,-0.712730901400849,0.577065441373076));
#7694=CARTESIAN_POINT('Ctrl Pts',(0.16675,-0.70196345051309,0.593445288500454));
#7695=CARTESIAN_POINT('Ctrl Pts',(0.16675,-0.69721937633955,0.600662150739582));
#7696=CARTESIAN_POINT('Ctrl Pts',(0.16675,-0.692374202308048,0.60781985304043));
#7697=CARTESIAN_POINT('Ctrl Pts',(0.16675,-0.687429007292474,0.614916081051289));
#7698=CARTESIAN_POINT('Ctrl Pts',(0.16675,-0.682714384849053,0.621681443334934));
#7699=CARTESIAN_POINT('Ctrl Pts',(0.16675,-0.677914372753535,0.628382975887117));
#7700=CARTESIAN_POINT('Ctrl Pts',(0.16675,-0.673031649136193,0.635017507597753));
#7701=CARTESIAN_POINT('Ctrl Pts',(0.16675,-0.647947101036107,0.669101810306574));
#7702=CARTESIAN_POINT('Ctrl Pts',(0.16675,-0.620675093575939,0.701430768012057));
#7703=CARTESIAN_POINT('Ctrl Pts',(0.16675,-0.591410629122804,0.731767455494602));
#7704=CARTESIAN_POINT('Ctrl Pts',(0.16675,-0.562349677540372,0.761893173582266));
#7705=CARTESIAN_POINT('Ctrl Pts',(0.16675,-0.531323346456511,0.790055413649179));
#7706=CARTESIAN_POINT('Ctrl Pts',(0.16675,-0.498475258847458,0.81600537002847));
#7707=CARTESIAN_POINT('Ctrl Pts',(0.16675,-0.474945639402752,0.834593745871793));
#7708=CARTESIAN_POINT('Ctrl Pts',(0.16675,-0.450480256842734,0.85204668515908));
#7709=CARTESIAN_POINT('Ctrl Pts',(0.16675,-0.425119128515106,0.868262223680471));
#7710=CARTESIAN_POINT('Ctrl Pts',(0.166750000000001,-0.430804868963497,
-0.601981847785733));
#7711=CARTESIAN_POINT('Ctrl Pts',(0.186567867725353,-0.243806898334343,
-0.734404661945218));
#7712=CARTESIAN_POINT('Ctrl Pts',(0.227601860671149,0.281971713823132,-0.817954447443626));
#7713=CARTESIAN_POINT('Ctrl Pts',(0.289851978837389,0.845141343193606,-0.223133510528201));
#7714=CARTESIAN_POINT('Ctrl Pts',(0.35350035449872,0.644441981350638,0.590684118087253));
#7715=CARTESIAN_POINT('Ctrl Pts',(0.417148730160053,-0.148625865295904,
0.86134357313186));
#7716=CARTESIAN_POINT('Ctrl Pts',(0.468072798427941,-0.673818062791027,
0.444668243636764));
#7717=CARTESIAN_POINT('Ctrl Pts',(0.497780741475386,-0.738435342237461,
0.0992847338226311));
#7718=CARTESIAN_POINT('Ctrl Pts',(0.506272559302387,-0.737970603191613,
0.000391387174775012));
#7719=CARTESIAN_POINT('Origin',(0.16675,-2.39206768658147E-16,-5.43753587379397E-17));
#7720=CARTESIAN_POINT('',(0.16675,-0.96675,-1.1839272930757E-16));
#7721=CARTESIAN_POINT('Origin',(0.16675,0.,0.));
#7722=CARTESIAN_POINT('Origin',(0.16675,0.,0.));
#7723=CARTESIAN_POINT('',(0.16675,0.429877377952346,-0.601104350279397));
#7724=CARTESIAN_POINT('Ctrl Pts',(0.16675,0.426126619158378,0.869594511950287));
#7725=CARTESIAN_POINT('Ctrl Pts',(0.16675,0.444048204157592,0.858234946722552));
#7726=CARTESIAN_POINT('Ctrl Pts',(0.16675,0.461543004418397,0.846256521223882));
#7727=CARTESIAN_POINT('Ctrl Pts',(0.16675,0.478574283244814,0.833657137809103));
#7728=CARTESIAN_POINT('Ctrl Pts',(0.16675,0.509001100399174,0.811148015662355));
#7729=CARTESIAN_POINT('Ctrl Pts',(0.16675,0.537950187081889,0.786657827653572));
#7730=CARTESIAN_POINT('Ctrl Pts',(0.16675,0.565322184247078,0.760390349102262));
#7731=CARTESIAN_POINT('Ctrl Pts',(0.16675,0.580977577122889,0.745366684804185));
#7732=CARTESIAN_POINT('Ctrl Pts',(0.16675,0.596116548389853,0.729761264861267));
#7733=CARTESIAN_POINT('Ctrl Pts',(0.16675,0.610716049466699,0.713610321391338));
#7734=CARTESIAN_POINT('Ctrl Pts',(0.16675,0.618614322575215,0.704872724002614));
#7735=CARTESIAN_POINT('Ctrl Pts',(0.16675,0.626355539003896,0.695974058824874));
#7736=CARTESIAN_POINT('Ctrl Pts',(0.16675,0.633922359419622,0.686936797568183));
#7737=CARTESIAN_POINT('Ctrl Pts',(0.16675,0.660736193525347,0.654912299721848));
#7738=CARTESIAN_POINT('Ctrl Pts',(0.16675,0.685405961021896,0.62110392557575));
#7739=CARTESIAN_POINT('Ctrl Pts',(0.16675,0.707789016811858,0.585785643849129));
#7740=CARTESIAN_POINT('Ctrl Pts',(0.16675,0.720604135012202,0.565564635636181));
#7741=CARTESIAN_POINT('Ctrl Pts',(0.16675,0.73266879088414,0.544848299455873));
#7742=CARTESIAN_POINT('Ctrl Pts',(0.16675,0.743948601837455,0.523686665378094));
#7743=CARTESIAN_POINT('Ctrl Pts',(0.16675,0.748254387048905,0.51560874178174));
#7744=CARTESIAN_POINT('Ctrl Pts',(0.16675,0.752445749108298,0.507465930781441));
#7745=CARTESIAN_POINT('Ctrl Pts',(0.16675,0.756520547836615,0.499261024570285));
#7746=CARTESIAN_POINT('Ctrl Pts',(0.16675,0.760218791127057,0.491814340361506));
#7747=CARTESIAN_POINT('Ctrl Pts',(0.16675,0.76381903212279,0.484320354352865));
#7748=CARTESIAN_POINT('Ctrl Pts',(0.16675,0.767316849163895,0.476788329033034));
#7749=CARTESIAN_POINT('Ctrl Pts',(0.16675,0.784221971045724,0.440385680022968));
#7750=CARTESIAN_POINT('Ctrl Pts',(0.16675,0.798763409678176,0.403045533144019));
#7751=CARTESIAN_POINT('Ctrl Pts',(0.16675,0.810809555762439,0.365012096556293));
#7752=CARTESIAN_POINT('Ctrl Pts',(0.16675,0.822574175743337,0.327867525596231));
#7753=CARTESIAN_POINT('Ctrl Pts',(0.16675,0.831958863643941,0.290060609212317));
#7754=CARTESIAN_POINT('Ctrl Pts',(0.16675,0.838792795668049,0.251820776324567));
#7755=CARTESIAN_POINT('Ctrl Pts',(0.16675,0.841943056397508,0.23419323138815));
#7756=CARTESIAN_POINT('Ctrl Pts',(0.16675,0.844550600272548,0.216473818776536));
#7757=CARTESIAN_POINT('Ctrl Pts',(0.16675,0.846595044183084,0.198686089961416));
#7758=CARTESIAN_POINT('Ctrl Pts',(0.16675,0.847632483705251,0.189659824781285));
#7759=CARTESIAN_POINT('Ctrl Pts',(0.16675,0.848524888038838,0.180615982855043));
#7760=CARTESIAN_POINT('Ctrl Pts',(0.16675,0.849269357780081,0.171557746034708));
#7761=CARTESIAN_POINT('Ctrl Pts',(0.16675,0.849858399166255,0.164390663106622));
#7762=CARTESIAN_POINT('Ctrl Pts',(0.16675,0.850354504412772,0.157217608502542));
#7763=CARTESIAN_POINT('Ctrl Pts',(0.16675,0.85075616472443,0.150048288143431));
#7764=CARTESIAN_POINT('Ctrl Pts',(0.16675,0.852777542388293,0.113968288157456));
#7765=CARTESIAN_POINT('Ctrl Pts',(0.16675,0.852415681074446,0.0779207678734099));
#7766=CARTESIAN_POINT('Ctrl Pts',(0.16675,0.849542285446746,0.0420946893478588));
#7767=CARTESIAN_POINT('Ctrl Pts',(0.16675,0.846888448693774,0.00900611533130068));
#7768=CARTESIAN_POINT('Ctrl Pts',(0.16675,0.842091236173531,-0.0238940214503569));
#7769=CARTESIAN_POINT('Ctrl Pts',(0.16675,0.835242858213107,-0.0564423061914987));
#7770=CARTESIAN_POINT('Ctrl Pts',(0.16675,0.828597188620167,-0.0880271789097645));
#7771=CARTESIAN_POINT('Ctrl Pts',(0.16675,0.820019479587032,-0.119281105396314));
#7772=CARTESIAN_POINT('Ctrl Pts',(0.16675,0.809574742100293,-0.150037087823665));
#7773=CARTESIAN_POINT('Ctrl Pts',(0.16675,0.806977307323436,-0.157685595835918));
#7774=CARTESIAN_POINT('Ctrl Pts',(0.16675,0.804266871727105,-0.165295576565078));
#7775=CARTESIAN_POINT('Ctrl Pts',(0.16675,0.801446902967295,-0.172859717658773));
#7776=CARTESIAN_POINT('Ctrl Pts',(0.16675,0.788417061552043,-0.207810303033373));
#7777=CARTESIAN_POINT('Ctrl Pts',(0.16675,0.773040216963918,-0.241819733336439));
#7778=CARTESIAN_POINT('Ctrl Pts',(0.16675,0.755459606524671,-0.27465734479009));
#7779=CARTESIAN_POINT('Ctrl Pts',(0.16675,0.738098146793609,-0.307085619728946));
#7780=CARTESIAN_POINT('Ctrl Pts',(0.16675,0.718586548468597,-0.338371978906755));
#7781=CARTESIAN_POINT('Ctrl Pts',(0.16675,0.697030730379467,-0.368255555684412));
#7782=CARTESIAN_POINT('Ctrl Pts',(0.16675,0.686837234519666,-0.382387151845577));
#7783=CARTESIAN_POINT('Ctrl Pts',(0.16675,0.676186226245501,-0.396204408183039));
#7784=CARTESIAN_POINT('Ctrl Pts',(0.16675,0.665087296091944,-0.409675840453131));
#7785=CARTESIAN_POINT('Ctrl Pts',(0.16675,0.659050486142239,-0.417003076073115));
#7786=CARTESIAN_POINT('Ctrl Pts',(0.16675,0.652878889824389,-0.424230235737168));
#7787=CARTESIAN_POINT('Ctrl Pts',(0.16675,0.646590889416737,-0.431333603793795));
#7788=CARTESIAN_POINT('Ctrl Pts',(0.16675,0.623179046694935,-0.457781269976265));
#7789=CARTESIAN_POINT('Ctrl Pts',(0.16675,0.598112400326066,-0.482571263352541));
#7790=CARTESIAN_POINT('Ctrl Pts',(0.16675,0.571498848118781,-0.505481850389779));
#7791=CARTESIAN_POINT('Ctrl Pts',(0.16675,0.545853275924679,-0.527559140534908));
#7792=CARTESIAN_POINT('Ctrl Pts',(0.16675,0.518770427098911,-0.547891640792012));
#7793=CARTESIAN_POINT('Ctrl Pts',(0.16675,0.490330976191895,-0.566236195677696));
#7794=CARTESIAN_POINT('Ctrl Pts',(0.16675,0.470811033951257,-0.578827319640305));
#7795=CARTESIAN_POINT('Ctrl Pts',(0.16675,0.450651674365123,-0.590480997499789));
#7796=CARTESIAN_POINT('Ctrl Pts',(0.16675,0.429877377952347,-0.601104350279396));
#7797=CARTESIAN_POINT('Origin',(0.16675,0.,0.));
#7798=CARTESIAN_POINT('Origin',(-0.572772559302386,0.,0.));
#7799=CARTESIAN_POINT('Ctrl Pts',(0.16675,0.429877377952346,-0.601104350279397));
#7800=CARTESIAN_POINT('Ctrl Pts',(0.187966125220444,0.63020268545344,-0.45784250583252));
#7801=CARTESIAN_POINT('Ctrl Pts',(0.230398375661332,0.872834123616866,0.0422493396134374));
#7802=CARTESIAN_POINT('Ctrl Pts',(0.294046751322663,0.435343216015217,0.758672715515329));
#7803=CARTESIAN_POINT('Ctrl Pts',(0.357695126983995,-0.402604296286284,
0.775582665152948));
#7804=CARTESIAN_POINT('Ctrl Pts',(0.402088690108978,-0.728851347662273,
0.291015012319514));
#7805=CARTESIAN_POINT('Ctrl Pts',(0.425266128013518,-0.740099388012232,
0.0231307056922991));
#7806=CARTESIAN_POINT('Ctrl Pts',(0.427227440697614,-0.739952215624596,
0.000448480265853929));
#7807=CARTESIAN_POINT('Ctrl Pts',(0.0352584761920628,0.562359885162963,
-0.786356739692297));
#7808=CARTESIAN_POINT('Ctrl Pts',(0.0564746014125067,0.824422795889191,
-0.59894349460567));
#7809=CARTESIAN_POINT('Ctrl Pts',(0.0989068518533945,1.14183002571936,0.0552700258068862));
#7810=CARTESIAN_POINT('Ctrl Pts',(0.162555227514726,0.56951022203344,0.992485585554051));
#7811=CARTESIAN_POINT('Ctrl Pts',(0.226203603176058,-0.526681601400223,
1.01460695742438));
#7812=CARTESIAN_POINT('Ctrl Pts',(0.289851978837389,-1.13858611742084,0.105758482516412));
#7813=CARTESIAN_POINT('Ctrl Pts',(0.353500354498721,-0.704219736298823,
-0.901062052194361));
#7814=CARTESIAN_POINT('Ctrl Pts',(0.417148730160052,0.377418552482973,-1.07936663274048));
#7815=CARTESIAN_POINT('Ctrl Pts',(0.480797105821384,1.11215948537616,-0.265909044073595));
#7816=CARTESIAN_POINT('Ctrl Pts',(0.544445481482716,0.824805026575853,0.792041364549834));
#7817=CARTESIAN_POINT('Ctrl Pts',(0.608093857144046,-0.220584842909833,
1.12201795069882));
#7818=CARTESIAN_POINT('Ctrl Pts',(0.67174223280538,-1.06324405762272,0.420851095111989));
#7819=CARTESIAN_POINT('Ctrl Pts',(0.735390608466709,-0.928746646791689,
-0.667109467222269));
#7820=CARTESIAN_POINT('Ctrl Pts',(0.799038984128042,0.0593036878978548,
-1.14196384784033));
#7821=CARTESIAN_POINT('Ctrl Pts',(0.862687359789374,0.992851037269299,-0.567317079889055));
#7822=CARTESIAN_POINT('Ctrl Pts',(0.926335735450704,1.01393309871856,0.528716826373647));
#7823=CARTESIAN_POINT('Ctrl Pts',(0.989984111112038,0.103174080250363,1.13883974488377));
#7824=CARTESIAN_POINT('Ctrl Pts',(1.05363248677337,-0.902405499999265,0.702328792682534));
#7825=CARTESIAN_POINT('Ctrl Pts',(1.1172808624347,-1.07864214409527,-0.379647872875257));
#7826=CARTESIAN_POINT('Ctrl Pts',(1.18092923809603,-0.263567945093874,-1.1127143000303));
#7827=CARTESIAN_POINT('Ctrl Pts',(1.24457761375736,0.793734598360108,-0.823156588847623));
#7828=CARTESIAN_POINT('Ctrl Pts',(1.30822598941869,1.12156665624076,0.222911765209374));
#7829=CARTESIAN_POINT('Ctrl Pts',(1.37187436508003,0.418638643118788,1.06411584982561));
#7830=CARTESIAN_POINT('Ctrl Pts',(1.43552274074136,-0.669033089544462,0.927359982025442));
#7831=CARTESIAN_POINT('Ctrl Pts',(1.49917111640269,-1.14183980758859,-0.0616741854150761));
#7832=CARTESIAN_POINT('Ctrl Pts',(1.56281949206402,-0.565254094904384,-0.994025233767431));
#7833=CARTESIAN_POINT('Ctrl Pts',(1.62646786772535,0.530819035010965,-1.01283588367238));
#7834=CARTESIAN_POINT('Ctrl Pts',(1.69011624338668,1.1390530241903,-0.100805646716435));
#7835=CARTESIAN_POINT('Ctrl Pts',(1.75376461904802,0.700451549597658,0.903852632500549));
#7836=CARTESIAN_POINT('Ctrl Pts',(1.81741299470935,-0.381880694848822,1.07786826185974));
#7837=CARTESIAN_POINT('Ctrl Pts',(1.88106137037068,-1.1132685844485,0.261226720517503));
#7838=CARTESIAN_POINT('Ctrl Pts',(1.94470974603201,-0.821489124128327,-0.795382116074246));
#7839=CARTESIAN_POINT('Ctrl Pts',(2.00835812169334,0.225204422399939,-1.12121417536036));
#7840=CARTESIAN_POINT('Ctrl Pts',(2.07200649735467,1.06504845822836,-0.416215070646207));
#7841=CARTESIAN_POINT('Ctrl Pts',(2.13565487301601,0.925843278457432,0.670548291357633));
#7842=CARTESIAN_POINT('Ctrl Pts',(2.19930324867734,-0.0637982312897449,
1.14249696551783));
#7843=CARTESIAN_POINT('Ctrl Pts',(2.26295162433867,-0.995715013444193,0.561588991513182));
#7844=CARTESIAN_POINT('Ctrl Pts',(2.30538387477956,-1.00549420213374,-0.165492191923457));
#7845=CARTESIAN_POINT('Ctrl Pts',(2.3266,-0.855344277194458,-0.450546035351206));
#7846=CARTESIAN_POINT('Ctrl Pts',(0.0790889841280419,0.51819904942609,-0.724605943221331));
#7847=CARTESIAN_POINT('Ctrl Pts',(0.100305109348486,0.759682759077274,-0.551909831681287));
#7848=CARTESIAN_POINT('Ctrl Pts',(0.142737359789374,1.05216472501853,0.050929797075736));
#7849=CARTESIAN_POINT('Ctrl Pts',(0.206385735450705,0.524787886694032,0.914547962207811));
#7850=CARTESIAN_POINT('Ctrl Pts',(0.270034111112037,-0.485322499695577,
0.934932193333899));
#7851=CARTESIAN_POINT('Ctrl Pts',(0.333682486773368,-1.04917555342029,0.0974535107404919));
#7852=CARTESIAN_POINT('Ctrl Pts',(0.3973308624347,-0.648918970867547,-0.830303709848955));
#7853=CARTESIAN_POINT('Ctrl Pts',(0.460979238096032,0.347780736664339,-0.994606439444508));
#7854=CARTESIAN_POINT('Ctrl Pts',(0.524627613757363,1.02482414435576,-0.245027814942394));
#7855=CARTESIAN_POINT('Ctrl Pts',(0.588275989418695,0.760034974062225,0.729844167488813));
#7856=CARTESIAN_POINT('Ctrl Pts',(0.651924365080026,-0.203262819645385,
1.03390844694167));
#7857=CARTESIAN_POINT('Ctrl Pts',(0.715572740741358,-0.979749933280485,
0.387802621045355));
#7858=CARTESIAN_POINT('Ctrl Pts',(0.77922111640269,-0.855814296543672,-0.614722886355148));
#7859=CARTESIAN_POINT('Ctrl Pts',(0.842869492064021,0.054646704907169,-1.05228803839437));
#7860=CARTESIAN_POINT('Ctrl Pts',(0.906517867725352,0.914884715835602,-0.522766966986812));
#7861=CARTESIAN_POINT('Ctrl Pts',(0.970166243386684,0.934311251211222,0.487197903106137));
#7862=CARTESIAN_POINT('Ctrl Pts',(1.03381461904802,0.0950720556741984,1.04940926409856));
#7863=CARTESIAN_POINT('Ctrl Pts',(1.09746299470935,-0.831541659770034,0.647176518729099));
#7864=CARTESIAN_POINT('Ctrl Pts',(1.16111137037068,-0.993938843235788,-0.349834993624386));
#7865=CARTESIAN_POINT('Ctrl Pts',(1.22475974603201,-0.242870557111759,-1.0253353906839));
#7866=CARTESIAN_POINT('Ctrl Pts',(1.28840812169334,0.731404435520177,-0.758515984379027));
#7867=CARTESIAN_POINT('Ctrl Pts',(1.35205649735468,1.03349259160535,0.205407014058117));
#7868=CARTESIAN_POINT('Ctrl Pts',(1.415704873016,0.385763907847585,0.980553265635359));
#7869=CARTESIAN_POINT('Ctrl Pts',(1.47935324867734,-0.616495451015456,0.854536523390396));
#7870=CARTESIAN_POINT('Ctrl Pts',(1.54300162433866,-1.05217373873994,-0.0568310526753888));
#7871=CARTESIAN_POINT('Ctrl Pts',(1.60665,-0.520865983495204,-0.915966705367969));
#7872=CARTESIAN_POINT('Ctrl Pts',(1.67029837566133,0.489135030106648,-0.933300197953434));
#7873=CARTESIAN_POINT('Ctrl Pts',(1.73394675132267,1.0496057950689,-0.0928896098093842));
#7874=CARTESIAN_POINT('Ctrl Pts',(1.79759512698399,0.645446691250665,0.832875152265396));
#7875=CARTESIAN_POINT('Ctrl Pts',(1.86124350264533,-0.351892477194545,0.993225732202447));
#7876=CARTESIAN_POINT('Ctrl Pts',(1.92489187830666,-1.02584614841431,0.240713183547288));
#7877=CARTESIAN_POINT('Ctrl Pts',(1.98854025396799,-0.756979461850859,-0.732922577435883));
#7878=CARTESIAN_POINT('Ctrl Pts',(2.05218862962932,0.20751963412252,-1.03316779024241));
#7879=CARTESIAN_POINT('Ctrl Pts',(2.11583700529065,0.981412638432993,-0.383530652978877));
#7880=CARTESIAN_POINT('Ctrl Pts',(2.17948538095198,0.853138923085075,0.617891667495313));
#7881=CARTESIAN_POINT('Ctrl Pts',(2.24313375661332,-0.0587883020849396,
1.05277929155983));
#7882=CARTESIAN_POINT('Ctrl Pts',(2.30678213227465,-0.917523790511027,0.517488692291692));
#7883=CARTESIAN_POINT('Ctrl Pts',(2.34921438271553,-0.926535041876538,-0.152496468551139));
#7884=CARTESIAN_POINT('Ctrl Pts',(2.37043050793598,-0.788176047169102,-0.415165685536108));
#7885=CARTESIAN_POINT('Ctrl Pts',(0.122919492064021,0.474038213689218,-0.662855146750364));
#7886=CARTESIAN_POINT('Ctrl Pts',(0.144135617284465,0.694942722265357,-0.504876168756904));
#7887=CARTESIAN_POINT('Ctrl Pts',(0.186567867725353,0.962499424317696,0.0465895683445864));
#7888=CARTESIAN_POINT('Ctrl Pts',(0.250216243386684,0.480065551354624,0.83661033886157));
#7889=CARTESIAN_POINT('Ctrl Pts',(0.313864619048015,-0.443963397990931,
0.855257429243423));
#7890=CARTESIAN_POINT('Ctrl Pts',(0.377512994709348,-0.959764989419737,
0.089148538964571));
#7891=CARTESIAN_POINT('Ctrl Pts',(0.441161370370679,-0.593618205436271,
-0.759545367503548));
#7892=CARTESIAN_POINT('Ctrl Pts',(0.504809746032011,0.318142920845704,-0.909846246148534));
#7893=CARTESIAN_POINT('Ctrl Pts',(0.568458121693342,0.937488803335355,-0.224146585811195));
#7894=CARTESIAN_POINT('Ctrl Pts',(0.632106497354674,0.695264921548596,0.667646970427793));
#7895=CARTESIAN_POINT('Ctrl Pts',(0.695754873016005,-0.185940796380938,
0.945798943184532));
#7896=CARTESIAN_POINT('Ctrl Pts',(0.759403248677337,-0.896255808938247,
0.35475414697872));
#7897=CARTESIAN_POINT('Ctrl Pts',(0.823051624338669,-0.782881946295657,
-0.562336305488026));
#7898=CARTESIAN_POINT('Ctrl Pts',(0.8867,0.049989721916484,-0.962612228948414));
#7899=CARTESIAN_POINT('Ctrl Pts',(0.950348375661331,0.836918394401904,-0.478216854084567));
#7900=CARTESIAN_POINT('Ctrl Pts',(1.01399675132266,0.854689403703885,0.445678979838627));
#7901=CARTESIAN_POINT('Ctrl Pts',(1.077645126984,0.0869700310980342,0.959978783313364));
#7902=CARTESIAN_POINT('Ctrl Pts',(1.14129350264533,-0.760677819540801,0.592024244775666));
#7903=CARTESIAN_POINT('Ctrl Pts',(1.20494187830666,-0.909235542376312,-0.320022114373516));
#7904=CARTESIAN_POINT('Ctrl Pts',(1.26859025396799,-0.222173169129643,-0.937956481337493));
#7905=CARTESIAN_POINT('Ctrl Pts',(1.33223862962932,0.669074272680244,-0.693875379910431));
#7906=CARTESIAN_POINT('Ctrl Pts',(1.39588700529065,0.945418526969947,0.18790226290686));
#7907=CARTESIAN_POINT('Ctrl Pts',(1.45953538095198,0.352889172576383,0.896990681445106));
#7908=CARTESIAN_POINT('Ctrl Pts',(1.52318375661332,-0.56395781248645,0.781713064755349));
#7909=CARTESIAN_POINT('Ctrl Pts',(1.58683213227465,-0.962507669891289,-0.0519879199356997));
#7910=CARTESIAN_POINT('Ctrl Pts',(1.65048050793598,-0.476477872086025,-0.837908176968511));
#7911=CARTESIAN_POINT('Ctrl Pts',(1.71412888359731,0.447451025202331,-0.853764512234482));
#7912=CARTESIAN_POINT('Ctrl Pts',(1.77777725925864,0.960158565947502,-0.0849735729023353));
#7913=CARTESIAN_POINT('Ctrl Pts',(1.84142563491997,0.590441832903672,0.761897672030244));
#7914=CARTESIAN_POINT('Ctrl Pts',(1.9050740105813,-0.321904259540268,0.908583202545158));
#7915=CARTESIAN_POINT('Ctrl Pts',(1.96872238624264,-0.938423712380128,0.220199646577074));
#7916=CARTESIAN_POINT('Ctrl Pts',(2.03237076190397,-0.692469799573391,-0.670463038797522));
#7917=CARTESIAN_POINT('Ctrl Pts',(2.0960191375653,0.189834845845101,-0.945121405124467));
#7918=CARTESIAN_POINT('Ctrl Pts',(2.15966751322663,0.897776818637627,-0.350846235311547));
#7919=CARTESIAN_POINT('Ctrl Pts',(2.22331588888796,0.780434567712718,0.565235043632989));
#7920=CARTESIAN_POINT('Ctrl Pts',(2.2869642645493,-0.0537783728801341,0.963061617601832));
#7921=CARTESIAN_POINT('Ctrl Pts',(2.35061264021062,-0.839332567577861,0.4733883930702));
#7922=CARTESIAN_POINT('Ctrl Pts',(2.39304489065151,-0.847575881619333,-0.13950074517882));
#7923=CARTESIAN_POINT('Ctrl Pts',(2.41426101587196,-0.721007817143747,-0.379785335721011));
#7924=CARTESIAN_POINT('Ctrl Pts',(0.16675,0.429877377952346,-0.601104350279397));
#7925=CARTESIAN_POINT('Ctrl Pts',(0.187966125220444,0.63020268545344,-0.45784250583252));
#7926=CARTESIAN_POINT('Ctrl Pts',(0.230398375661332,0.872834123616866,0.0422493396134374));
#7927=CARTESIAN_POINT('Ctrl Pts',(0.294046751322663,0.435343216015217,0.758672715515329));
#7928=CARTESIAN_POINT('Ctrl Pts',(0.357695126983995,-0.402604296286284,
0.775582665152948));
#7929=CARTESIAN_POINT('Ctrl Pts',(0.421343502645327,-0.870354425419187,
0.0808435671886495));
#7930=CARTESIAN_POINT('Ctrl Pts',(0.484991878306658,-0.538317440004995,
-0.688787025158141));
#7931=CARTESIAN_POINT('Ctrl Pts',(0.54864025396799,0.288505105027068,-0.825086052852563));
#7932=CARTESIAN_POINT('Ctrl Pts',(0.612288629629321,0.850153462314954,-0.203265356679994));
#7933=CARTESIAN_POINT('Ctrl Pts',(0.675937005290653,0.630494869034967,0.605449773366773));
#7934=CARTESIAN_POINT('Ctrl Pts',(0.739585380951984,-0.168618773116491,
0.857689439427387));
#7935=CARTESIAN_POINT('Ctrl Pts',(0.803233756613316,-0.81276168459601,0.321705672912086));
#7936=CARTESIAN_POINT('Ctrl Pts',(0.866882132274647,-0.70994959604764,-0.509949724620904));
#7937=CARTESIAN_POINT('Ctrl Pts',(0.93053050793598,0.0453327389257982,-0.872936419502457));
#7938=CARTESIAN_POINT('Ctrl Pts',(0.99417888359731,0.758952072968206,-0.433666741182324));
#7939=CARTESIAN_POINT('Ctrl Pts',(1.05782725925864,0.775067556196549,0.404160056571117));
#7940=CARTESIAN_POINT('Ctrl Pts',(1.12147563491997,0.0788680065218695,0.870548302528163));
#7941=CARTESIAN_POINT('Ctrl Pts',(1.1851240105813,-0.689813979311569,0.536871970822231));
#7942=CARTESIAN_POINT('Ctrl Pts',(1.24877238624264,-0.824532241516836,-0.290209235122645));
#7943=CARTESIAN_POINT('Ctrl Pts',(1.31242076190396,-0.201475781147527,-0.850577571991093));
#7944=CARTESIAN_POINT('Ctrl Pts',(1.37606913756531,0.606744109840312,-0.629234775441834));
#7945=CARTESIAN_POINT('Ctrl Pts',(1.43971751322663,0.857344462334542,0.170397511755603));
#7946=CARTESIAN_POINT('Ctrl Pts',(1.50336588888797,0.32001443730518,0.813428097254852));
#7947=CARTESIAN_POINT('Ctrl Pts',(1.56701426454929,-0.511420173957444,0.708889606120302));
#7948=CARTESIAN_POINT('Ctrl Pts',(1.63066264021063,-0.872841601042637,-0.0471447871960115));
#7949=CARTESIAN_POINT('Ctrl Pts',(1.69431101587196,-0.432089760676844,-0.759849648569051));
#7950=CARTESIAN_POINT('Ctrl Pts',(1.75795939153329,0.405767020298013,-0.774228826515532));
#7951=CARTESIAN_POINT('Ctrl Pts',(1.82160776719462,0.870711336826102,-0.0770575359952864));
#7952=CARTESIAN_POINT('Ctrl Pts',(1.88525614285595,0.535436974556678,0.690920191795093));
#7953=CARTESIAN_POINT('Ctrl Pts',(1.94890451851728,-0.291916041885991,0.823940672887867));
#7954=CARTESIAN_POINT('Ctrl Pts',(2.01255289417862,-0.851001276345943,0.199686109606861));
#7955=CARTESIAN_POINT('Ctrl Pts',(2.07620126983995,-0.627960137295923,-0.60800350015916));
#7956=CARTESIAN_POINT('Ctrl Pts',(2.13984964550128,0.172150057567682,-0.857075020006521));
#7957=CARTESIAN_POINT('Ctrl Pts',(2.20349802116261,0.814140998842262,-0.318161817644216));
#7958=CARTESIAN_POINT('Ctrl Pts',(2.26714639682394,0.707730212340359,0.512578419770666));
#7959=CARTESIAN_POINT('Ctrl Pts',(2.33079477248527,-0.0487684436753277,
0.873343943643834));
#7960=CARTESIAN_POINT('Ctrl Pts',(2.39444314814661,-0.761141344644696,0.429288093848709));
#7961=CARTESIAN_POINT('Ctrl Pts',(2.43687539858749,-0.768616721362127,-0.126505021806502));
#7962=CARTESIAN_POINT('Ctrl Pts',(2.45809152380794,-0.653839587118391,-0.344404985905914));
#7963=CARTESIAN_POINT('Ctrl Pts',(2.3266,-0.855344277194458,-0.450546035351206));
#7964=CARTESIAN_POINT('Ctrl Pts',(2.31631197229656,-0.928154301239586,-0.312319011910983));
#7965=CARTESIAN_POINT('Ctrl Pts',(2.30602394459312,-0.964507862952725,-0.155636376663986));
#7966=CARTESIAN_POINT('Ctrl Pts',(2.29573591688968,-0.964651808581398,0.000865815094782327));
#7967=CARTESIAN_POINT('Origin',(0.,-9.54517714852416E-17,-0.519615242270663));
#7968=CARTESIAN_POINT('',(0.,-9.54517714852416E-17,-0.519615242270663));
#7969=CARTESIAN_POINT('',(0.,0.45,-0.259807621135332));
#7970=CARTESIAN_POINT('',(0.,0.4125,-0.281458256229943));
#7971=CARTESIAN_POINT('',(1.2,-6.93889390390723E-17,-0.519615242270663));
#7972=CARTESIAN_POINT('',(0.,-9.54517714852416E-17,-0.519615242270663));
#7973=CARTESIAN_POINT('',(1.2,0.45,-0.259807621135332));
#7974=CARTESIAN_POINT('',(1.2,-9.54517714852416E-17,-0.519615242270663));
#7975=CARTESIAN_POINT('',(0.,0.45,-0.259807621135332));
#7976=CARTESIAN_POINT('Origin',(0.,-0.45,-0.259807621135332));
#7977=CARTESIAN_POINT('',(0.,-0.45,-0.259807621135332));
#7978=CARTESIAN_POINT('',(0.,-0.0375000000000001,-0.497964607176052));
#7979=CARTESIAN_POINT('',(1.2,-0.45,-0.259807621135332));
#7980=CARTESIAN_POINT('',(0.,-0.45,-0.259807621135332));
#7981=CARTESIAN_POINT('',(1.2,-0.45,-0.259807621135332));
#7982=CARTESIAN_POINT('Origin',(0.,-0.45,0.259807621135332));
#7983=CARTESIAN_POINT('',(0.,-0.45,0.259807621135332));
#7984=CARTESIAN_POINT('',(0.,-0.45,0.129903810567666));
#7985=CARTESIAN_POINT('',(1.2,-0.45,0.259807621135332));
#7986=CARTESIAN_POINT('',(0.,-0.45,0.259807621135332));
#7987=CARTESIAN_POINT('',(1.2,-0.45,0.259807621135332));
#7988=CARTESIAN_POINT('Origin',(0.,3.18172571617472E-17,0.519615242270663));
#7989=CARTESIAN_POINT('',(0.,3.18172571617472E-17,0.519615242270663));
#7990=CARTESIAN_POINT('',(0.,0.1875,0.627868417743718));
#7991=CARTESIAN_POINT('',(1.2,0.,0.519615242270663));
#7992=CARTESIAN_POINT('',(0.,3.18172571617472E-17,0.519615242270663));
#7993=CARTESIAN_POINT('',(1.2,3.18172571617472E-17,0.519615242270663));
#7994=CARTESIAN_POINT('Origin',(0.,0.45,0.259807621135332));
#7995=CARTESIAN_POINT('',(0.,0.45,0.259807621135332));
#7996=CARTESIAN_POINT('',(0.,0.6375,0.151554445662277));
#7997=CARTESIAN_POINT('',(1.2,0.45,0.259807621135332));
#7998=CARTESIAN_POINT('',(0.,0.45,0.259807621135332));
#7999=CARTESIAN_POINT('',(1.2,0.45,0.259807621135332));
#8000=CARTESIAN_POINT('Origin',(0.,0.45,-0.259807621135332));
#8001=CARTESIAN_POINT('',(0.,0.45,-0.129903810567666));
#8002=CARTESIAN_POINT('',(1.2,0.45,-0.259807621135332));
#8003=CARTESIAN_POINT('Origin',(1.2,0.,-6.93889390390723E-17));
#8004=CARTESIAN_POINT('Origin',(0.,0.8,0.));
#8005=CARTESIAN_POINT('',(6.93889390390723E-17,-0.8,-9.79717439317883E-17));
#8006=CARTESIAN_POINT('Origin',(0.,0.,0.));
#8007=CARTESIAN_POINT('Origin',(0.1,0.,0.));
#8008=CARTESIAN_POINT('',(0.1,-0.9,-1.10218211923262E-16));
#8009=CARTESIAN_POINT('Origin',(1.25,0.,0.));
#8010=CARTESIAN_POINT('Origin',(2.3266,0.,0.));
#8011=CARTESIAN_POINT('Origin',(2.4,0.,0.));
#8012=CARTESIAN_POINT('',(2.5,-0.75,-9.18485099360515E-17));
#8013=CARTESIAN_POINT('Origin',(2.5,0.,0.));
#8014=CARTESIAN_POINT('',(2.4,-0.875,-1.07156594925393E-16));
#8015=CARTESIAN_POINT('Origin',(2.5,0.,0.));
#11409=UNCERTAINTY_MEASURE_WITH_UNIT(LENGTH_MEASURE(0.01),#11431,
'DISTANCE_ACCURACY_VALUE',
'Maximum model space distance between geometric entities at asserted c
onnectivities');
#11416=UNCERTAINTY_MEASURE_WITH_UNIT(LENGTH_MEASURE(0.01),#11431,
'DISTANCE_ACCURACY_VALUE',
'Maximum model space distance between geometric entities at asserted c
onnectivities');
#11423=(
GEOMETRIC_REPRESENTATION_CONTEXT(3)
GLOBAL_UNCERTAINTY_ASSIGNED_CONTEXT((#11409))
GLOBAL_UNIT_ASSIGNED_CONTEXT((#11431,#11433,#11434))
REPRESENTATION_CONTEXT('','3D')
);
#11430=(
GEOMETRIC_REPRESENTATION_CONTEXT(3)
GLOBAL_UNCERTAINTY_ASSIGNED_CONTEXT((#11416))
GLOBAL_UNIT_ASSIGNED_CONTEXT((#11431,#11433,#11434))
REPRESENTATION_CONTEXT('','3D')
);
#11431=(
LENGTH_UNIT()
NAMED_UNIT(*)
SI_UNIT(.MILLI.,.METRE.)
);
#11433=(
NAMED_UNIT(*)
PLANE_ANGLE_UNIT()
SI_UNIT($,.RADIAN.)
);
#11434=(
NAMED_UNIT(*)
SI_UNIT($,.STERADIAN.)
SOLID_ANGLE_UNIT()
);
#11441=SHAPE_DEFINITION_REPRESENTATION(#11454,#11484);
#11454=PRODUCT_DEFINITION_SHAPE('',$,#11498);
#11484=SHAPE_REPRESENTATION('',(#4806),#11423);
#11491=PRODUCT_DEFINITION_CONTEXT('part definition',#11532,'design');
#11498=PRODUCT_DEFINITION('2026-10-25-00-55-38-514',
'06_Set_Screw_ISO_4026_M2x2.5',#11511,#11491);
#11511=PRODUCT_DEFINITION_FORMATION('',$,#11540);
#11532=APPLICATION_CONTEXT(
'Core Data for Automotive Mechanical Design Process');
#11533=PRODUCT_CONTEXT('part definition',#11532,'mechanical');
#11540=PRODUCT('2026-10-25-00-55-38-514','06_Set_Screw_ISO_4026_M2x2.5',
$,(#11533));
#11610=COLOUR_RGB('Black',0.12,0.14,0.17);
#11611=FILL_AREA_STYLE_COLOUR('',#11610);
#11612=FILL_AREA_STYLE('',(#11611));
#11613=SURFACE_STYLE_FILL_AREA(#11612);
#11614=SURFACE_SIDE_STYLE('',(#11613));
#11615=SURFACE_STYLE_USAGE(.BOTH.,#11614);
#11616=PRESENTATION_STYLE_ASSIGNMENT((#11615));
ENDSEC;
END-ISO-10303-21;
